ISO-10303-21;
HEADER;
/* Generated by software containing ST-Developer
 * from STEP Tools, Inc. (www.steptools.com) 
 */

FILE_DESCRIPTION(
/* description */ ('Bearing friction torque test rig'),
/* implementation_level */ '2;1');

FILE_NAME(
/* name */ 'Cage (1).step',
/* time_stamp */ '2026-10-28T03:24:04-07:00',
/* author */ (''),
/* organization */ (''),
/* preprocessor_version */ 'ST-DEVELOPER v20.2',
/* originating_system */ 'Autodesk Translation Framework v15.17.0.0',
/* authorisation */ '');

FILE_SCHEMA (('AUTOMOTIVE_DESIGN { 1 0 10303 214 3 1 1 }'));
ENDSEC;

DATA;
#10=MECHANICAL_DESIGN_GEOMETRIC_PRESENTATION_REPRESENTATION('',(#577),#14822);
#357=B_SPLINE_CURVE_WITH_KNOTS('',3,(#13426,#13427,#13428,#13429,#13430,
#13431,#13432,#13433,#13434,#13435,#13436,#13437,#13438,#13439,#13440,#13441,
#13442,#13443,#13444,#13445,#13446,#13447),.UNSPECIFIED.,.F.,.F.,(4,2,2,
2,2,2,2,2,2,2,4),(0.0789094028588958,0.210573405340968,0.315860108011452,
0.421146810681936,0.522142632548711,0.623138454415485,0.72413427628226,
0.825130098149035,0.930416800819519,1.03570350349,1.16736750597208),
 .UNSPECIFIED.);
#358=B_SPLINE_CURVE_WITH_KNOTS('',3,(#13451,#13452,#13453,#13454,#13455,
#13456,#13457,#13458,#13459,#13460,#13461,#13462,#13463,#13464,#13465,#13466,
#13467,#13468,#13469,#13470,#13471,#13472),.UNSPECIFIED.,.F.,.F.,(4,2,2,
2,2,2,2,2,2,2,4),(0.0774793363974613,0.142088896491891,0.284177792983782,
0.411119756996526,0.514392970548519,0.617666184100513,0.720939397652506,
0.8242126112045,0.951154575217244,1.09324347170913,1.15785303180356),
 .UNSPECIFIED.);
#359=B_SPLINE_CURVE_WITH_KNOTS('',3,(#13478,#13479,#13480,#13481,#13482,
#13483,#13484,#13485,#13486,#13487,#13488,#13489,#13490,#13491,#13492,#13493,
#13494,#13495,#13496,#13497,#13498,#13499),.UNSPECIFIED.,.F.,.F.,(4,2,2,
2,2,2,2,2,2,2,4),(0.0774793363974613,0.142088896491891,0.284177792983782,
0.411119756996525,0.514392970548519,0.617666184100513,0.720939397652506,
0.8242126112045,0.951154575217243,1.09324347170913,1.15785303180356),
 .UNSPECIFIED.);
#360=B_SPLINE_CURVE_WITH_KNOTS('',3,(#13503,#13504,#13505,#13506,#13507,
#13508,#13509,#13510,#13511,#13512,#13513,#13514,#13515,#13516,#13517,#13518,
#13519,#13520,#13521,#13522,#13523,#13524),.UNSPECIFIED.,.F.,.F.,(4,2,2,
2,2,2,2,2,2,2,4),(0.0774793363974614,0.142088896491891,0.284177792983781,
0.411119756996525,0.514392970548519,0.617666184100512,0.720939397652506,
0.824212611204499,0.951154575217243,1.09324347170913,1.15785303180356),
 .UNSPECIFIED.);
#361=B_SPLINE_CURVE_WITH_KNOTS('',3,(#13528,#13529,#13530,#13531,#13532,
#13533,#13534,#13535,#13536,#13537,#13538,#13539),.UNSPECIFIED.,.F.,.F.,
(4,2,2,2,2,4),(0.0774793363974613,0.142088896491891,0.284177792983781,0.411119756996525,
0.514392970548519,0.617666184100512),.UNSPECIFIED.);
#362=B_SPLINE_CURVE_WITH_KNOTS('',3,(#13544,#13545,#13546,#13547,#13548,
#13549,#13550,#13551,#13552,#13553,#13554,#13555),.UNSPECIFIED.,.F.,.F.,
(4,2,2,2,2,4),(0.617666184100512,0.720939397652506,0.824212611204499,0.951154575217243,
1.09324347170913,1.15785303180356),.UNSPECIFIED.);
#363=B_SPLINE_CURVE_WITH_KNOTS('',3,(#13559,#13560,#13561,#13562,#13563,
#13564,#13565,#13566,#13567,#13568,#13569,#13570,#13571,#13572,#13573,#13574,
#13575,#13576,#13577,#13578,#13579,#13580),.UNSPECIFIED.,.F.,.F.,(4,2,2,
2,2,2,2,2,2,2,4),(0.0774793363974613,0.142088896491891,0.284177792983782,
0.411119756996526,0.514392970548519,0.617666184100513,0.720939397652507,
0.8242126112045,0.951154575217245,1.09324347170914,1.15785303180356),
 .UNSPECIFIED.);
#364=B_SPLINE_CURVE_WITH_KNOTS('',3,(#13584,#13585,#13586,#13587,#13588,
#13589,#13590,#13591,#13592,#13593,#13594,#13595,#13596,#13597,#13598,#13599,
#13600,#13601,#13602,#13603,#13604,#13605),.UNSPECIFIED.,.F.,.F.,(4,2,2,
2,2,2,2,2,2,2,4),(0.0774793363974613,0.142088896491891,0.284177792983782,
0.411119756996526,0.514392970548519,0.617666184100513,0.720939397652506,
0.824212611204499,0.951154575217243,1.09324347170913,1.15785303180356),
 .UNSPECIFIED.);
#365=B_SPLINE_CURVE_WITH_KNOTS('',3,(#13609,#13610,#13611,#13612,#13613,
#13614,#13615,#13616,#13617,#13618,#13619,#13620,#13621,#13622,#13623,#13624,
#13625,#13626,#13627,#13628,#13629,#13630),.UNSPECIFIED.,.F.,.F.,(4,2,2,
2,2,2,2,2,2,2,4),(0.0774793363974613,0.142088896491891,0.284177792983782,
0.411119756996526,0.514392970548519,0.617666184100513,0.720939397652506,
0.8242126112045,0.951154575217244,1.09324347170913,1.15785303180356),
 .UNSPECIFIED.);
#366=B_SPLINE_CURVE_WITH_KNOTS('',3,(#13634,#13635,#13636,#13637,#13638,
#13639,#13640,#13641,#13642,#13643,#13644,#13645,#13646,#13647,#13648,#13649,
#13650,#13651,#13652,#13653,#13654,#13655),.UNSPECIFIED.,.F.,.F.,(4,2,2,
2,2,2,2,2,2,2,4),(0.0774793363974613,0.142088896491891,0.284177792983782,
0.411119756996526,0.514392970548519,0.617666184100513,0.720939397652506,
0.8242126112045,0.951154575217243,1.09324347170913,1.15785303180356),
 .UNSPECIFIED.);
#367=B_SPLINE_CURVE_WITH_KNOTS('',3,(#13663,#13664,#13665,#13666,#13667,
#13668,#13669,#13670,#13671,#13672,#13673,#13674,#13675,#13676,#13677,#13678,
#13679,#13680,#13681,#13682,#13683,#13684),.UNSPECIFIED.,.F.,.F.,(4,2,2,
2,2,2,2,2,2,2,4),(0.0789094028588958,0.210573405340968,0.315860108011452,
0.421146810681936,0.522142632548711,0.623138454415485,0.72413427628226,
0.825130098149035,0.930416800819519,1.03570350349,1.16736750597208),
 .UNSPECIFIED.);
#368=B_SPLINE_CURVE_WITH_KNOTS('',3,(#13692,#13693,#13694,#13695,#13696,
#13697,#13698,#13699,#13700,#13701,#13702,#13703,#13704,#13705,#13706,#13707,
#13708,#13709,#13710,#13711,#13712,#13713),.UNSPECIFIED.,.F.,.F.,(4,2,2,
2,2,2,2,2,2,2,4),(0.0789094028588958,0.210573405340969,0.315860108011453,
0.421146810681937,0.522142632548712,0.623138454415486,0.724134276282261,
0.825130098149035,0.930416800819519,1.03570350349,1.16736750597208),
 .UNSPECIFIED.);
#369=B_SPLINE_CURVE_WITH_KNOTS('',3,(#13722,#13723,#13724,#13725,#13726,
#13727,#13728,#13729,#13730,#13731,#13732,#13733),.UNSPECIFIED.,.F.,.F.,
(4,2,2,2,2,4),(0.0789094028588958,0.210573405340968,0.315860108011452,0.421146810681937,
0.522142632548711,0.623138454415486),.UNSPECIFIED.);
#370=B_SPLINE_CURVE_WITH_KNOTS('',3,(#13735,#13736,#13737,#13738,#13739,
#13740,#13741,#13742,#13743,#13744,#13745,#13746),.UNSPECIFIED.,.F.,.F.,
(4,2,2,2,2,4),(0.623138454415486,0.72413427628226,0.825130098149035,0.930416800819519,
1.03570350349,1.16736750597208),.UNSPECIFIED.);
#371=B_SPLINE_CURVE_WITH_KNOTS('',3,(#13753,#13754,#13755,#13756,#13757,
#13758,#13759,#13760,#13761,#13762,#13763,#13764,#13765,#13766,#13767,#13768,
#13769,#13770,#13771,#13772,#13773,#13774),.UNSPECIFIED.,.F.,.F.,(4,2,2,
2,2,2,2,2,2,2,4),(0.0789094028588958,0.210573405340968,0.315860108011452,
0.421146810681936,0.522142632548711,0.623138454415486,0.72413427628226,
0.825130098149035,0.930416800819519,1.03570350349,1.16736750597208),
 .UNSPECIFIED.);
#372=B_SPLINE_CURVE_WITH_KNOTS('',3,(#13782,#13783,#13784,#13785,#13786,
#13787,#13788,#13789,#13790,#13791,#13792,#13793,#13794,#13795,#13796,#13797,
#13798,#13799,#13800,#13801,#13802,#13803),.UNSPECIFIED.,.F.,.F.,(4,2,2,
2,2,2,2,2,2,2,4),(0.0789094028588957,0.210573405340968,0.315860108011452,
0.421146810681936,0.522142632548711,0.623138454415485,0.72413427628226,
0.825130098149035,0.930416800819519,1.03570350349,1.16736750597207),
 .UNSPECIFIED.);
#373=B_SPLINE_CURVE_WITH_KNOTS('',3,(#13811,#13812,#13813,#13814,#13815,
#13816,#13817,#13818,#13819,#13820,#13821,#13822,#13823,#13824,#13825,#13826,
#13827,#13828,#13829,#13830,#13831,#13832),.UNSPECIFIED.,.F.,.F.,(4,2,2,
2,2,2,2,2,2,2,4),(0.0789094028588958,0.210573405340968,0.315860108011452,
0.421146810681936,0.522142632548711,0.623138454415486,0.72413427628226,
0.825130098149035,0.930416800819519,1.03570350349,1.16736750597208),
 .UNSPECIFIED.);
#374=B_SPLINE_CURVE_WITH_KNOTS('',3,(#13841,#13842,#13843,#13844,#13845,
#13846,#13847,#13848,#13849,#13850,#13851,#13852,#13853,#13854,#13855,#13856,
#13857,#13858,#13859,#13860,#13861,#13862),.UNSPECIFIED.,.F.,.F.,(4,2,2,
2,2,2,2,2,2,2,4),(0.0789094028588958,0.210573405340968,0.315860108011452,
0.421146810681936,0.522142632548711,0.623138454415485,0.72413427628226,
0.825130098149035,0.930416800819519,1.03570350349,1.16736750597208),
 .UNSPECIFIED.);
#417=SPHERICAL_SURFACE('',#8809,0.412776);
#418=SPHERICAL_SURFACE('',#8825,0.412776);
#419=SPHERICAL_SURFACE('',#8830,0.412776);
#420=SPHERICAL_SURFACE('',#8835,0.412776);
#421=SPHERICAL_SURFACE('',#8840,0.412776);
#422=SPHERICAL_SURFACE('',#8845,0.412776);
#423=SPHERICAL_SURFACE('',#8850,0.412776);
#424=SPHERICAL_SURFACE('',#8858,0.412776);
#485=SHAPE_REPRESENTATION_RELATIONSHIP('SRR','None',#15026,#524);
#524=ADVANCED_BREP_SHAPE_REPRESENTATION('',(#630),#14806);
#577=STYLED_ITEM('',(#15284),#630);
#630=MANIFOLD_SOLID_BREP('Continuous crown cage',#7694);
#827=FACE_BOUND('',#2054,.T.);
#1022=PLANE('',#8822);
#1023=PLANE('',#8827);
#1024=PLANE('',#8832);
#1025=PLANE('',#8837);
#1026=PLANE('',#8842);
#1027=PLANE('',#8847);
#1028=PLANE('',#8856);
#1029=PLANE('',#8860);
#1030=PLANE('',#8861);
#1408=FACE_OUTER_BOUND('',#2036,.T.);
#1409=FACE_OUTER_BOUND('',#2037,.T.);
#1410=FACE_OUTER_BOUND('',#2038,.T.);
#1411=FACE_OUTER_BOUND('',#2039,.T.);
#1412=FACE_OUTER_BOUND('',#2040,.T.);
#1413=FACE_OUTER_BOUND('',#2041,.T.);
#1414=FACE_OUTER_BOUND('',#2042,.T.);
#1415=FACE_OUTER_BOUND('',#2043,.T.);
#1416=FACE_OUTER_BOUND('',#2044,.T.);
#1417=FACE_OUTER_BOUND('',#2045,.T.);
#1418=FACE_OUTER_BOUND('',#2046,.T.);
#1419=FACE_OUTER_BOUND('',#2047,.T.);
#1420=FACE_OUTER_BOUND('',#2048,.T.);
#1421=FACE_OUTER_BOUND('',#2049,.T.);
#1422=FACE_OUTER_BOUND('',#2050,.T.);
#1423=FACE_OUTER_BOUND('',#2051,.T.);
#1424=FACE_OUTER_BOUND('',#2052,.T.);
#1425=FACE_OUTER_BOUND('',#2053,.T.);
#1426=FACE_OUTER_BOUND('',#2055,.T.);
#2036=EDGE_LOOP('',(#6482,#6483,#6484,#6485));
#2037=EDGE_LOOP('',(#6486,#6487,#6488,#6489,#6490,#6491,#6492,#6493,#6494,
#6495,#6496,#6497,#6498,#6499,#6500,#6501,#6502,#6503,#6504,#6505));
#2038=EDGE_LOOP('',(#6506,#6507,#6508,#6509));
#2039=EDGE_LOOP('',(#6510,#6511,#6512,#6513));
#2040=EDGE_LOOP('',(#6514,#6515,#6516,#6517));
#2041=EDGE_LOOP('',(#6518,#6519,#6520,#6521));
#2042=EDGE_LOOP('',(#6522,#6523,#6524,#6525));
#2043=EDGE_LOOP('',(#6526,#6527,#6528,#6529,#6530,#6531));
#2044=EDGE_LOOP('',(#6532,#6533,#6534,#6535));
#2045=EDGE_LOOP('',(#6536,#6537,#6538,#6539));
#2046=EDGE_LOOP('',(#6540,#6541,#6542,#6543));
#2047=EDGE_LOOP('',(#6544,#6545,#6546,#6547));
#2048=EDGE_LOOP('',(#6548,#6549,#6550,#6551));
#2049=EDGE_LOOP('',(#6552,#6553,#6554,#6555));
#2050=EDGE_LOOP('',(#6556,#6557,#6558,#6559,#6560,#6561,#6562,#6563,#6564,
#6565,#6566,#6567,#6568,#6569,#6570,#6571,#6572,#6573,#6574,#6575));
#2051=EDGE_LOOP('',(#6576,#6577,#6578,#6579));
#2052=EDGE_LOOP('',(#6580,#6581,#6582,#6583));
#2053=EDGE_LOOP('',(#6584));
#2054=EDGE_LOOP('',(#6585));
#2055=EDGE_LOOP('',(#6586,#6587,#6588,#6589));
#2548=LINE('',#13541,#2992);
#2549=LINE('',#13837,#2993);
#2992=VECTOR('',#10843,1.706752);
#2993=VECTOR('',#10920,1.643248);
#3425=CIRCLE('',#8810,0.405071403305639);
#3426=CIRCLE('',#8811,0.405071403305639);
#3427=CIRCLE('',#8813,1.706752);
#3428=CIRCLE('',#8814,1.706752);
#3429=CIRCLE('',#8815,1.706752);
#3430=CIRCLE('',#8816,1.706752);
#3431=CIRCLE('',#8817,1.706752);
#3432=CIRCLE('',#8818,1.706752);
#3433=CIRCLE('',#8819,1.706752);
#3434=CIRCLE('',#8820,1.706752);
#3435=CIRCLE('',#8821,1.706752);
#3436=CIRCLE('',#8823,1.643248);
#3437=CIRCLE('',#8824,0.405071403305639);
#3438=CIRCLE('',#8826,0.405071403305639);
#3439=CIRCLE('',#8828,1.643248);
#3440=CIRCLE('',#8829,0.405071403305639);
#3441=CIRCLE('',#8831,0.405071403305639);
#3442=CIRCLE('',#8833,1.643248);
#3443=CIRCLE('',#8834,0.405071403305639);
#3444=CIRCLE('',#8836,0.405071403305639);
#3445=CIRCLE('',#8838,1.643248);
#3446=CIRCLE('',#8839,0.405071403305639);
#3447=CIRCLE('',#8841,0.405071403305639);
#3448=CIRCLE('',#8843,1.643248);
#3449=CIRCLE('',#8844,0.405071403305639);
#3450=CIRCLE('',#8846,0.405071403305639);
#3451=CIRCLE('',#8848,1.643248);
#3452=CIRCLE('',#8849,0.405071403305639);
#3453=CIRCLE('',#8851,0.405071403305639);
#3454=CIRCLE('',#8853,1.643248);
#3455=CIRCLE('',#8854,1.643248);
#3456=CIRCLE('',#8855,1.643248);
#3457=CIRCLE('',#8857,0.405071403305639);
#3458=CIRCLE('',#8859,0.405071403305639);
#4014=VERTEX_POINT('',#13424);
#4015=VERTEX_POINT('',#13425);
#4016=VERTEX_POINT('',#13448);
#4017=VERTEX_POINT('',#13450);
#4018=VERTEX_POINT('',#13475);
#4019=VERTEX_POINT('',#13477);
#4020=VERTEX_POINT('',#13500);
#4021=VERTEX_POINT('',#13502);
#4022=VERTEX_POINT('',#13525);
#4023=VERTEX_POINT('',#13527);
#4024=VERTEX_POINT('',#13540);
#4025=VERTEX_POINT('',#13543);
#4026=VERTEX_POINT('',#13556);
#4027=VERTEX_POINT('',#13558);
#4028=VERTEX_POINT('',#13581);
#4029=VERTEX_POINT('',#13583);
#4030=VERTEX_POINT('',#13606);
#4031=VERTEX_POINT('',#13608);
#4032=VERTEX_POINT('',#13631);
#4033=VERTEX_POINT('',#13633);
#4034=VERTEX_POINT('',#13658);
#4035=VERTEX_POINT('',#13662);
#4036=VERTEX_POINT('',#13687);
#4037=VERTEX_POINT('',#13691);
#4038=VERTEX_POINT('',#13716);
#4039=VERTEX_POINT('',#13720);
#4040=VERTEX_POINT('',#13721);
#4041=VERTEX_POINT('',#13748);
#4042=VERTEX_POINT('',#13752);
#4043=VERTEX_POINT('',#13777);
#4044=VERTEX_POINT('',#13781);
#4045=VERTEX_POINT('',#13806);
#4046=VERTEX_POINT('',#13810);
#4047=VERTEX_POINT('',#13835);
#4048=VERTEX_POINT('',#13838);
#4049=VERTEX_POINT('',#13840);
#4867=EDGE_CURVE('',#4014,#4015,#357,.T.);
#4868=EDGE_CURVE('',#4016,#4014,#3425,.T.);
#4869=EDGE_CURVE('',#4017,#4016,#358,.T.);
#4870=EDGE_CURVE('',#4015,#4017,#3426,.T.);
#4871=EDGE_CURVE('',#4018,#4016,#3427,.T.);
#4872=EDGE_CURVE('',#4018,#4019,#359,.T.);
#4873=EDGE_CURVE('',#4020,#4019,#3428,.T.);
#4874=EDGE_CURVE('',#4020,#4021,#360,.T.);
#4875=EDGE_CURVE('',#4022,#4021,#3429,.T.);
#4876=EDGE_CURVE('',#4022,#4023,#361,.T.);
#4877=EDGE_CURVE('',#4023,#4024,#2548,.T.);
#4878=EDGE_CURVE('',#4024,#4024,#3430,.T.);
#4879=EDGE_CURVE('',#4023,#4025,#362,.T.);
#4880=EDGE_CURVE('',#4026,#4025,#3431,.T.);
#4881=EDGE_CURVE('',#4026,#4027,#363,.T.);
#4882=EDGE_CURVE('',#4028,#4027,#3432,.T.);
#4883=EDGE_CURVE('',#4028,#4029,#364,.T.);
#4884=EDGE_CURVE('',#4030,#4029,#3433,.T.);
#4885=EDGE_CURVE('',#4030,#4031,#365,.T.);
#4886=EDGE_CURVE('',#4032,#4031,#3434,.T.);
#4887=EDGE_CURVE('',#4032,#4033,#366,.T.);
#4888=EDGE_CURVE('',#4017,#4033,#3435,.T.);
#4889=EDGE_CURVE('',#4014,#4034,#3436,.T.);
#4890=EDGE_CURVE('',#4034,#4018,#3437,.T.);
#4891=EDGE_CURVE('',#4035,#4034,#367,.T.);
#4892=EDGE_CURVE('',#4019,#4035,#3438,.T.);
#4893=EDGE_CURVE('',#4035,#4036,#3439,.T.);
#4894=EDGE_CURVE('',#4036,#4020,#3440,.T.);
#4895=EDGE_CURVE('',#4037,#4036,#368,.T.);
#4896=EDGE_CURVE('',#4021,#4037,#3441,.T.);
#4897=EDGE_CURVE('',#4037,#4038,#3442,.T.);
#4898=EDGE_CURVE('',#4038,#4022,#3443,.T.);
#4899=EDGE_CURVE('',#4039,#4040,#369,.T.);
#4900=EDGE_CURVE('',#4025,#4039,#3444,.T.);
#4901=EDGE_CURVE('',#4040,#4038,#370,.T.);
#4902=EDGE_CURVE('',#4039,#4041,#3445,.T.);
#4903=EDGE_CURVE('',#4041,#4026,#3446,.T.);
#4904=EDGE_CURVE('',#4042,#4041,#371,.T.);
#4905=EDGE_CURVE('',#4027,#4042,#3447,.T.);
#4906=EDGE_CURVE('',#4042,#4043,#3448,.T.);
#4907=EDGE_CURVE('',#4043,#4028,#3449,.T.);
#4908=EDGE_CURVE('',#4044,#4043,#372,.T.);
#4909=EDGE_CURVE('',#4029,#4044,#3450,.T.);
#4910=EDGE_CURVE('',#4044,#4045,#3451,.T.);
#4911=EDGE_CURVE('',#4045,#4030,#3452,.T.);
#4912=EDGE_CURVE('',#4046,#4045,#373,.T.);
#4913=EDGE_CURVE('',#4031,#4046,#3453,.T.);
#4914=EDGE_CURVE('',#4047,#4047,#3454,.T.);
#4915=EDGE_CURVE('',#4047,#4040,#2549,.T.);
#4916=EDGE_CURVE('',#4048,#4015,#3455,.T.);
#4917=EDGE_CURVE('',#4048,#4049,#374,.T.);
#4918=EDGE_CURVE('',#4046,#4049,#3456,.T.);
#4919=EDGE_CURVE('',#4033,#4048,#3457,.T.);
#4920=EDGE_CURVE('',#4049,#4032,#3458,.T.);
#6482=ORIENTED_EDGE('',*,*,#4867,.F.);
#6483=ORIENTED_EDGE('',*,*,#4868,.F.);
#6484=ORIENTED_EDGE('',*,*,#4869,.F.);
#6485=ORIENTED_EDGE('',*,*,#4870,.F.);
#6486=ORIENTED_EDGE('',*,*,#4869,.T.);
#6487=ORIENTED_EDGE('',*,*,#4871,.F.);
#6488=ORIENTED_EDGE('',*,*,#4872,.T.);
#6489=ORIENTED_EDGE('',*,*,#4873,.F.);
#6490=ORIENTED_EDGE('',*,*,#4874,.T.);
#6491=ORIENTED_EDGE('',*,*,#4875,.F.);
#6492=ORIENTED_EDGE('',*,*,#4876,.T.);
#6493=ORIENTED_EDGE('',*,*,#4877,.T.);
#6494=ORIENTED_EDGE('',*,*,#4878,.F.);
#6495=ORIENTED_EDGE('',*,*,#4877,.F.);
#6496=ORIENTED_EDGE('',*,*,#4879,.T.);
#6497=ORIENTED_EDGE('',*,*,#4880,.F.);
#6498=ORIENTED_EDGE('',*,*,#4881,.T.);
#6499=ORIENTED_EDGE('',*,*,#4882,.F.);
#6500=ORIENTED_EDGE('',*,*,#4883,.T.);
#6501=ORIENTED_EDGE('',*,*,#4884,.F.);
#6502=ORIENTED_EDGE('',*,*,#4885,.T.);
#6503=ORIENTED_EDGE('',*,*,#4886,.F.);
#6504=ORIENTED_EDGE('',*,*,#4887,.T.);
#6505=ORIENTED_EDGE('',*,*,#4888,.F.);
#6506=ORIENTED_EDGE('',*,*,#4868,.T.);
#6507=ORIENTED_EDGE('',*,*,#4889,.T.);
#6508=ORIENTED_EDGE('',*,*,#4890,.T.);
#6509=ORIENTED_EDGE('',*,*,#4871,.T.);
#6510=ORIENTED_EDGE('',*,*,#4891,.F.);
#6511=ORIENTED_EDGE('',*,*,#4892,.F.);
#6512=ORIENTED_EDGE('',*,*,#4872,.F.);
#6513=ORIENTED_EDGE('',*,*,#4890,.F.);
#6514=ORIENTED_EDGE('',*,*,#4892,.T.);
#6515=ORIENTED_EDGE('',*,*,#4893,.T.);
#6516=ORIENTED_EDGE('',*,*,#4894,.T.);
#6517=ORIENTED_EDGE('',*,*,#4873,.T.);
#6518=ORIENTED_EDGE('',*,*,#4895,.F.);
#6519=ORIENTED_EDGE('',*,*,#4896,.F.);
#6520=ORIENTED_EDGE('',*,*,#4874,.F.);
#6521=ORIENTED_EDGE('',*,*,#4894,.F.);
#6522=ORIENTED_EDGE('',*,*,#4896,.T.);
#6523=ORIENTED_EDGE('',*,*,#4897,.T.);
#6524=ORIENTED_EDGE('',*,*,#4898,.T.);
#6525=ORIENTED_EDGE('',*,*,#4875,.T.);
#6526=ORIENTED_EDGE('',*,*,#4899,.F.);
#6527=ORIENTED_EDGE('',*,*,#4900,.F.);
#6528=ORIENTED_EDGE('',*,*,#4879,.F.);
#6529=ORIENTED_EDGE('',*,*,#4876,.F.);
#6530=ORIENTED_EDGE('',*,*,#4898,.F.);
#6531=ORIENTED_EDGE('',*,*,#4901,.F.);
#6532=ORIENTED_EDGE('',*,*,#4900,.T.);
#6533=ORIENTED_EDGE('',*,*,#4902,.T.);
#6534=ORIENTED_EDGE('',*,*,#4903,.T.);
#6535=ORIENTED_EDGE('',*,*,#4880,.T.);
#6536=ORIENTED_EDGE('',*,*,#4904,.F.);
#6537=ORIENTED_EDGE('',*,*,#4905,.F.);
#6538=ORIENTED_EDGE('',*,*,#4881,.F.);
#6539=ORIENTED_EDGE('',*,*,#4903,.F.);
#6540=ORIENTED_EDGE('',*,*,#4905,.T.);
#6541=ORIENTED_EDGE('',*,*,#4906,.T.);
#6542=ORIENTED_EDGE('',*,*,#4907,.T.);
#6543=ORIENTED_EDGE('',*,*,#4882,.T.);
#6544=ORIENTED_EDGE('',*,*,#4908,.F.);
#6545=ORIENTED_EDGE('',*,*,#4909,.F.);
#6546=ORIENTED_EDGE('',*,*,#4883,.F.);
#6547=ORIENTED_EDGE('',*,*,#4907,.F.);
#6548=ORIENTED_EDGE('',*,*,#4909,.T.);
#6549=ORIENTED_EDGE('',*,*,#4910,.T.);
#6550=ORIENTED_EDGE('',*,*,#4911,.T.);
#6551=ORIENTED_EDGE('',*,*,#4884,.T.);
#6552=ORIENTED_EDGE('',*,*,#4885,.F.);
#6553=ORIENTED_EDGE('',*,*,#4911,.F.);
#6554=ORIENTED_EDGE('',*,*,#4912,.F.);
#6555=ORIENTED_EDGE('',*,*,#4913,.F.);
#6556=ORIENTED_EDGE('',*,*,#4914,.F.);
#6557=ORIENTED_EDGE('',*,*,#4915,.T.);
#6558=ORIENTED_EDGE('',*,*,#4901,.T.);
#6559=ORIENTED_EDGE('',*,*,#4897,.F.);
#6560=ORIENTED_EDGE('',*,*,#4895,.T.);
#6561=ORIENTED_EDGE('',*,*,#4893,.F.);
#6562=ORIENTED_EDGE('',*,*,#4891,.T.);
#6563=ORIENTED_EDGE('',*,*,#4889,.F.);
#6564=ORIENTED_EDGE('',*,*,#4867,.T.);
#6565=ORIENTED_EDGE('',*,*,#4916,.F.);
#6566=ORIENTED_EDGE('',*,*,#4917,.T.);
#6567=ORIENTED_EDGE('',*,*,#4918,.F.);
#6568=ORIENTED_EDGE('',*,*,#4912,.T.);
#6569=ORIENTED_EDGE('',*,*,#4910,.F.);
#6570=ORIENTED_EDGE('',*,*,#4908,.T.);
#6571=ORIENTED_EDGE('',*,*,#4906,.F.);
#6572=ORIENTED_EDGE('',*,*,#4904,.T.);
#6573=ORIENTED_EDGE('',*,*,#4902,.F.);
#6574=ORIENTED_EDGE('',*,*,#4899,.T.);
#6575=ORIENTED_EDGE('',*,*,#4915,.F.);
#6576=ORIENTED_EDGE('',*,*,#4870,.T.);
#6577=ORIENTED_EDGE('',*,*,#4888,.T.);
#6578=ORIENTED_EDGE('',*,*,#4919,.T.);
#6579=ORIENTED_EDGE('',*,*,#4916,.T.);
#6580=ORIENTED_EDGE('',*,*,#4887,.F.);
#6581=ORIENTED_EDGE('',*,*,#4920,.F.);
#6582=ORIENTED_EDGE('',*,*,#4917,.F.);
#6583=ORIENTED_EDGE('',*,*,#4919,.F.);
#6584=ORIENTED_EDGE('',*,*,#4878,.T.);
#6585=ORIENTED_EDGE('',*,*,#4914,.T.);
#6586=ORIENTED_EDGE('',*,*,#4913,.T.);
#6587=ORIENTED_EDGE('',*,*,#4918,.T.);
#6588=ORIENTED_EDGE('',*,*,#4920,.T.);
#6589=ORIENTED_EDGE('',*,*,#4886,.T.);
#7168=CYLINDRICAL_SURFACE('',#8812,1.706752);
#7169=CYLINDRICAL_SURFACE('',#8852,1.643248);
#7519=ADVANCED_FACE('',(#1408),#417,.F.);
#7520=ADVANCED_FACE('',(#1409),#7168,.T.);
#7521=ADVANCED_FACE('',(#1410),#1022,.T.);
#7522=ADVANCED_FACE('',(#1411),#418,.F.);
#7523=ADVANCED_FACE('',(#1412),#1023,.T.);
#7524=ADVANCED_FACE('',(#1413),#419,.F.);
#7525=ADVANCED_FACE('',(#1414),#1024,.T.);
#7526=ADVANCED_FACE('',(#1415),#420,.F.);
#7527=ADVANCED_FACE('',(#1416),#1025,.T.);
#7528=ADVANCED_FACE('',(#1417),#421,.F.);
#7529=ADVANCED_FACE('',(#1418),#1026,.T.);
#7530=ADVANCED_FACE('',(#1419),#422,.F.);
#7531=ADVANCED_FACE('',(#1420),#1027,.T.);
#7532=ADVANCED_FACE('',(#1421),#423,.F.);
#7533=ADVANCED_FACE('',(#1422),#7169,.F.);
#7534=ADVANCED_FACE('',(#1423),#1028,.T.);
#7535=ADVANCED_FACE('',(#1424),#424,.F.);
#7536=ADVANCED_FACE('',(#1425,#827),#1029,.T.);
#7537=ADVANCED_FACE('',(#1426),#1030,.T.);
#7694=CLOSED_SHELL('',(#7519,#7520,#7521,#7522,#7523,#7524,#7525,#7526,
#7527,#7528,#7529,#7530,#7531,#7532,#7533,#7534,#7535,#7536,#7537));
#8808=AXIS2_PLACEMENT_3D('',#13422,#10827,#10828);
#8809=AXIS2_PLACEMENT_3D('',#13423,#10829,#10830);
#8810=AXIS2_PLACEMENT_3D('',#13449,#10831,#10832);
#8811=AXIS2_PLACEMENT_3D('',#13473,#10833,#10834);
#8812=AXIS2_PLACEMENT_3D('',#13474,#10835,#10836);
#8813=AXIS2_PLACEMENT_3D('',#13476,#10837,#10838);
#8814=AXIS2_PLACEMENT_3D('',#13501,#10839,#10840);
#8815=AXIS2_PLACEMENT_3D('',#13526,#10841,#10842);
#8816=AXIS2_PLACEMENT_3D('',#13542,#10844,#10845);
#8817=AXIS2_PLACEMENT_3D('',#13557,#10846,#10847);
#8818=AXIS2_PLACEMENT_3D('',#13582,#10848,#10849);
#8819=AXIS2_PLACEMENT_3D('',#13607,#10850,#10851);
#8820=AXIS2_PLACEMENT_3D('',#13632,#10852,#10853);
#8821=AXIS2_PLACEMENT_3D('',#13656,#10854,#10855);
#8822=AXIS2_PLACEMENT_3D('',#13657,#10856,#10857);
#8823=AXIS2_PLACEMENT_3D('',#13659,#10858,#10859);
#8824=AXIS2_PLACEMENT_3D('',#13660,#10860,#10861);
#8825=AXIS2_PLACEMENT_3D('',#13661,#10862,#10863);
#8826=AXIS2_PLACEMENT_3D('',#13685,#10864,#10865);
#8827=AXIS2_PLACEMENT_3D('',#13686,#10866,#10867);
#8828=AXIS2_PLACEMENT_3D('',#13688,#10868,#10869);
#8829=AXIS2_PLACEMENT_3D('',#13689,#10870,#10871);
#8830=AXIS2_PLACEMENT_3D('',#13690,#10872,#10873);
#8831=AXIS2_PLACEMENT_3D('',#13714,#10874,#10875);
#8832=AXIS2_PLACEMENT_3D('',#13715,#10876,#10877);
#8833=AXIS2_PLACEMENT_3D('',#13717,#10878,#10879);
#8834=AXIS2_PLACEMENT_3D('',#13718,#10880,#10881);
#8835=AXIS2_PLACEMENT_3D('',#13719,#10882,#10883);
#8836=AXIS2_PLACEMENT_3D('',#13734,#10884,#10885);
#8837=AXIS2_PLACEMENT_3D('',#13747,#10886,#10887);
#8838=AXIS2_PLACEMENT_3D('',#13749,#10888,#10889);
#8839=AXIS2_PLACEMENT_3D('',#13750,#10890,#10891);
#8840=AXIS2_PLACEMENT_3D('',#13751,#10892,#10893);
#8841=AXIS2_PLACEMENT_3D('',#13775,#10894,#10895);
#8842=AXIS2_PLACEMENT_3D('',#13776,#10896,#10897);
#8843=AXIS2_PLACEMENT_3D('',#13778,#10898,#10899);
#8844=AXIS2_PLACEMENT_3D('',#13779,#10900,#10901);
#8845=AXIS2_PLACEMENT_3D('',#13780,#10902,#10903);
#8846=AXIS2_PLACEMENT_3D('',#13804,#10904,#10905);
#8847=AXIS2_PLACEMENT_3D('',#13805,#10906,#10907);
#8848=AXIS2_PLACEMENT_3D('',#13807,#10908,#10909);
#8849=AXIS2_PLACEMENT_3D('',#13808,#10910,#10911);
#8850=AXIS2_PLACEMENT_3D('',#13809,#10912,#10913);
#8851=AXIS2_PLACEMENT_3D('',#13833,#10914,#10915);
#8852=AXIS2_PLACEMENT_3D('',#13834,#10916,#10917);
#8853=AXIS2_PLACEMENT_3D('',#13836,#10918,#10919);
#8854=AXIS2_PLACEMENT_3D('',#13839,#10921,#10922);
#8855=AXIS2_PLACEMENT_3D('',#13863,#10923,#10924);
#8856=AXIS2_PLACEMENT_3D('',#13864,#10925,#10926);
#8857=AXIS2_PLACEMENT_3D('',#13865,#10927,#10928);
#8858=AXIS2_PLACEMENT_3D('',#13866,#10929,#10930);
#8859=AXIS2_PLACEMENT_3D('',#13867,#10931,#10932);
#8860=AXIS2_PLACEMENT_3D('',#13868,#10933,#10934);
#8861=AXIS2_PLACEMENT_3D('',#13869,#10935,#10936);
#10827=DIRECTION('axis',(0.,0.,1.));
#10828=DIRECTION('refdir',(1.,0.,0.));
#10829=DIRECTION('center_axis',(0.,0.,1.));
#10830=DIRECTION('ref_axis',(1.,0.,0.));
#10831=DIRECTION('center_axis',(0.,-1.,0.));
#10832=DIRECTION('ref_axis',(0.,0.,-1.));
#10833=DIRECTION('center_axis',(0.,-1.,0.));
#10834=DIRECTION('ref_axis',(0.,0.,-1.));
#10835=DIRECTION('center_axis',(0.,1.,0.));
#10836=DIRECTION('ref_axis',(1.,0.,0.));
#10837=DIRECTION('center_axis',(0.,1.,0.));
#10838=DIRECTION('ref_axis',(1.,0.,0.));
#10839=DIRECTION('center_axis',(0.,1.,0.));
#10840=DIRECTION('ref_axis',(1.,0.,0.));
#10841=DIRECTION('center_axis',(0.,1.,0.));
#10842=DIRECTION('ref_axis',(1.,0.,0.));
#10843=DIRECTION('',(0.,-1.,0.));
#10844=DIRECTION('center_axis',(0.,-1.,0.));
#10845=DIRECTION('ref_axis',(1.,0.,0.));
#10846=DIRECTION('center_axis',(0.,1.,0.));
#10847=DIRECTION('ref_axis',(1.,0.,0.));
#10848=DIRECTION('center_axis',(0.,1.,0.));
#10849=DIRECTION('ref_axis',(1.,0.,0.));
#10850=DIRECTION('center_axis',(0.,1.,0.));
#10851=DIRECTION('ref_axis',(1.,0.,0.));
#10852=DIRECTION('center_axis',(0.,1.,0.));
#10853=DIRECTION('ref_axis',(1.,0.,0.));
#10854=DIRECTION('center_axis',(0.,1.,0.));
#10855=DIRECTION('ref_axis',(1.,0.,0.));
#10856=DIRECTION('center_axis',(0.,1.,0.));
#10857=DIRECTION('ref_axis',(1.,0.,0.));
#10858=DIRECTION('center_axis',(0.,-1.,0.));
#10859=DIRECTION('ref_axis',(1.,0.,0.));
#10860=DIRECTION('center_axis',(0.,-1.,0.));
#10861=DIRECTION('ref_axis',(0.,0.,-1.));
#10862=DIRECTION('center_axis',(6.12323399573677E-17,0.,1.));
#10863=DIRECTION('ref_axis',(1.,0.,0.));
#10864=DIRECTION('center_axis',(0.,-1.,0.));
#10865=DIRECTION('ref_axis',(0.,0.,-1.));
#10866=DIRECTION('center_axis',(0.,1.,0.));
#10867=DIRECTION('ref_axis',(1.,0.,0.));
#10868=DIRECTION('center_axis',(0.,-1.,0.));
#10869=DIRECTION('ref_axis',(1.,0.,0.));
#10870=DIRECTION('center_axis',(0.,-1.,0.));
#10871=DIRECTION('ref_axis',(0.,0.,-1.));
#10872=DIRECTION('center_axis',(0.,0.,1.));
#10873=DIRECTION('ref_axis',(1.,0.,0.));
#10874=DIRECTION('center_axis',(0.,-1.,0.));
#10875=DIRECTION('ref_axis',(0.,0.,-1.));
#10876=DIRECTION('center_axis',(0.,1.,0.));
#10877=DIRECTION('ref_axis',(1.,0.,0.));
#10878=DIRECTION('center_axis',(0.,-1.,0.));
#10879=DIRECTION('ref_axis',(1.,0.,0.));
#10880=DIRECTION('center_axis',(0.,-1.,0.));
#10881=DIRECTION('ref_axis',(0.,0.,-1.));
#10882=DIRECTION('center_axis',(0.,0.,1.));
#10883=DIRECTION('ref_axis',(1.,0.,0.));
#10884=DIRECTION('center_axis',(0.,-1.,0.));
#10885=DIRECTION('ref_axis',(0.,0.,-1.));
#10886=DIRECTION('center_axis',(0.,1.,0.));
#10887=DIRECTION('ref_axis',(1.,0.,0.));
#10888=DIRECTION('center_axis',(0.,-1.,0.));
#10889=DIRECTION('ref_axis',(1.,0.,0.));
#10890=DIRECTION('center_axis',(0.,-1.,0.));
#10891=DIRECTION('ref_axis',(0.,0.,-1.));
#10892=DIRECTION('center_axis',(0.,0.,1.));
#10893=DIRECTION('ref_axis',(1.,0.,0.));
#10894=DIRECTION('center_axis',(0.,-1.,0.));
#10895=DIRECTION('ref_axis',(0.,0.,-1.));
#10896=DIRECTION('center_axis',(0.,1.,0.));
#10897=DIRECTION('ref_axis',(1.,0.,0.));
#10898=DIRECTION('center_axis',(0.,-1.,0.));
#10899=DIRECTION('ref_axis',(1.,0.,0.));
#10900=DIRECTION('center_axis',(0.,-1.,0.));
#10901=DIRECTION('ref_axis',(0.,0.,-1.));
#10902=DIRECTION('center_axis',(6.12323399573676E-17,0.,1.));
#10903=DIRECTION('ref_axis',(1.,0.,0.));
#10904=DIRECTION('center_axis',(0.,-1.,0.));
#10905=DIRECTION('ref_axis',(0.,0.,-1.));
#10906=DIRECTION('center_axis',(0.,1.,0.));
#10907=DIRECTION('ref_axis',(1.,0.,0.));
#10908=DIRECTION('center_axis',(0.,-1.,0.));
#10909=DIRECTION('ref_axis',(1.,0.,0.));
#10910=DIRECTION('center_axis',(0.,-1.,0.));
#10911=DIRECTION('ref_axis',(0.,0.,-1.));
#10912=DIRECTION('center_axis',(0.,0.,1.));
#10913=DIRECTION('ref_axis',(1.,0.,0.));
#10914=DIRECTION('center_axis',(0.,-1.,0.));
#10915=DIRECTION('ref_axis',(0.,0.,-1.));
#10916=DIRECTION('center_axis',(0.,1.,0.));
#10917=DIRECTION('ref_axis',(1.,0.,0.));
#10918=DIRECTION('center_axis',(0.,1.,0.));
#10919=DIRECTION('ref_axis',(1.,0.,0.));
#10920=DIRECTION('',(0.,1.,0.));
#10921=DIRECTION('center_axis',(0.,-1.,0.));
#10922=DIRECTION('ref_axis',(1.,0.,0.));
#10923=DIRECTION('center_axis',(0.,-1.,0.));
#10924=DIRECTION('ref_axis',(1.,0.,0.));
#10925=DIRECTION('center_axis',(0.,1.,0.));
#10926=DIRECTION('ref_axis',(1.,0.,0.));
#10927=DIRECTION('center_axis',(0.,-1.,0.));
#10928=DIRECTION('ref_axis',(0.,0.,-1.));
#10929=DIRECTION('center_axis',(0.,0.,1.));
#10930=DIRECTION('ref_axis',(1.,0.,0.));
#10931=DIRECTION('center_axis',(0.,-1.,0.));
#10932=DIRECTION('ref_axis',(0.,0.,-1.));
#10933=DIRECTION('center_axis',(0.,-1.,0.));
#10934=DIRECTION('ref_axis',(-1.,0.,0.));
#10935=DIRECTION('center_axis',(0.,1.,0.));
#10936=DIRECTION('ref_axis',(1.,0.,0.));
#13422=CARTESIAN_POINT('',(0.,0.,0.));
#13423=CARTESIAN_POINT('Origin',(1.18440385848747,0.,1.18440385848747));
#13424=CARTESIAN_POINT('',(0.846804978391753,-0.07938,1.40825612658882));
#13425=CARTESIAN_POINT('',(1.40825612658882,-0.07938,0.846804978391754));
#13426=CARTESIAN_POINT('Ctrl Pts',(0.846804978391752,-0.0793800000000001,
1.40825612658882));
#13427=CARTESIAN_POINT('Ctrl Pts',(0.854205272175554,-0.123401821157026,
1.40380622184538));
#13428=CARTESIAN_POINT('Ctrl Pts',(0.867957148219441,-0.166543350814306,
1.39550172959303));
#13429=CARTESIAN_POINT('Ctrl Pts',(0.902193646979982,-0.237231147975234,
1.3735491215176));
#13430=CARTESIAN_POINT('Ctrl Pts',(0.920778333482564,-0.266264900654909,
1.36127834356734));
#13431=CARTESIAN_POINT('Ctrl Pts',(0.962485392528369,-0.317195968905306,
1.33211611256184));
#13432=CARTESIAN_POINT('Ctrl Pts',(0.985600426557816,-0.33909093068465,
1.31521005565926));
#13433=CARTESIAN_POINT('Ctrl Pts',(1.03253285680459,-0.373586846396559,
1.27866649102984));
#13434=CARTESIAN_POINT('Ctrl Pts',(1.05871835910697,-0.388086240756494,
1.25722555095714));
#13435=CARTESIAN_POINT('Ctrl Pts',(1.11153475808518,-0.407068917407805,
1.2107812086231));
#13436=CARTESIAN_POINT('Ctrl Pts',(1.13814686046673,-0.411552957311693,
1.18575674747573));
#13437=CARTESIAN_POINT('Ctrl Pts',(1.18575674747573,-0.411552957311693,
1.13814686046673));
#13438=CARTESIAN_POINT('Ctrl Pts',(1.2107812086231,-0.407068917407805,1.11153475808518));
#13439=CARTESIAN_POINT('Ctrl Pts',(1.25722555095713,-0.388086240756494,
1.05871835910697));
#13440=CARTESIAN_POINT('Ctrl Pts',(1.27866649102984,-0.373586846396559,
1.03253285680459));
#13441=CARTESIAN_POINT('Ctrl Pts',(1.31521005565926,-0.33909093068465,0.985600426557816));
#13442=CARTESIAN_POINT('Ctrl Pts',(1.33211611256184,-0.317195968905306,
0.962485392528369));
#13443=CARTESIAN_POINT('Ctrl Pts',(1.36127834356734,-0.266264900654909,
0.920778333482565));
#13444=CARTESIAN_POINT('Ctrl Pts',(1.3735491215176,-0.237231147975234,0.902193646979983));
#13445=CARTESIAN_POINT('Ctrl Pts',(1.39550172959303,-0.166543350814306,
0.867957148219442));
#13446=CARTESIAN_POINT('Ctrl Pts',(1.40380622184538,-0.123401821157026,
0.854205272175555));
#13447=CARTESIAN_POINT('Ctrl Pts',(1.40825612658882,-0.0793800000000001,
0.846804978391753));
#13448=CARTESIAN_POINT('',(0.886256117232623,-0.07938,1.45861320581289));
#13449=CARTESIAN_POINT('Origin',(1.18440385848747,-0.07938,1.18440385848747));
#13450=CARTESIAN_POINT('',(1.45861320581289,-0.07938,0.886256117232624));
#13451=CARTESIAN_POINT('Ctrl Pts',(1.45861320581289,-0.0793800000000001,
0.886256117232623));
#13452=CARTESIAN_POINT('Ctrl Pts',(1.45630208793976,-0.101649918886749,
0.890059788636852));
#13453=CARTESIAN_POINT('Ctrl Pts',(1.45296717977858,-0.123823518623746,
0.895520212222107));
#13454=CARTESIAN_POINT('Ctrl Pts',(1.43904931717599,-0.192480977588836,
0.917859913453975));
#13455=CARTESIAN_POINT('Ctrl Pts',(1.4243271592157,-0.236152929235938,0.940896403863072));
#13456=CARTESIAN_POINT('Ctrl Pts',(1.39055359345152,-0.303141259068212,
0.990027513266106));
#13457=CARTESIAN_POINT('Ctrl Pts',(1.36743459453896,-0.335108247315849,
1.02199477007745));
#13458=CARTESIAN_POINT('Ctrl Pts',(1.32643091652006,-0.373243761060364,
1.07446535104584));
#13459=CARTESIAN_POINT('Ctrl Pts',(1.30441816675528,-0.387888272594439,
1.10126842659597));
#13460=CARTESIAN_POINT('Ctrl Pts',(1.25681160160691,-0.407041111792943,
1.15530234155453));
#13461=CARTESIAN_POINT('Ctrl Pts',(1.23119764287622,-0.411552957311693,
1.18251418313119));
#13462=CARTESIAN_POINT('Ctrl Pts',(1.18251418313119,-0.411552957311693,
1.23119764287622));
#13463=CARTESIAN_POINT('Ctrl Pts',(1.15530234155453,-0.407041111792943,
1.25681160160691));
#13464=CARTESIAN_POINT('Ctrl Pts',(1.10126842659597,-0.387888272594439,
1.30441816675528));
#13465=CARTESIAN_POINT('Ctrl Pts',(1.07446535104584,-0.373243761060364,
1.32643091652006));
#13466=CARTESIAN_POINT('Ctrl Pts',(1.02199477007745,-0.335108247315848,
1.36743459453896));
#13467=CARTESIAN_POINT('Ctrl Pts',(0.990027513266105,-0.303141259068211,
1.39055359345152));
#13468=CARTESIAN_POINT('Ctrl Pts',(0.940896403863071,-0.236152929235937,
1.42432715921571));
#13469=CARTESIAN_POINT('Ctrl Pts',(0.917859913453974,-0.192480977588835,
1.43904931717599));
#13470=CARTESIAN_POINT('Ctrl Pts',(0.895520212222106,-0.123823518623745,
1.45296717977858));
#13471=CARTESIAN_POINT('Ctrl Pts',(0.890059788636851,-0.101649918886749,
1.45630208793976));
#13472=CARTESIAN_POINT('Ctrl Pts',(0.886256117232622,-0.0793800000000001,
1.45861320581289));
#13473=CARTESIAN_POINT('Origin',(1.18440385848747,-0.07938,1.18440385848747));
#13474=CARTESIAN_POINT('Origin',(0.,-0.27783,0.));
#13475=CARTESIAN_POINT('',(0.404717578595295,-0.07938,1.65807299932179));
#13476=CARTESIAN_POINT('Origin',(0.,-0.07938,0.));
#13477=CARTESIAN_POINT('',(-0.404717578595296,-0.07938,1.65807299932179));
#13478=CARTESIAN_POINT('Ctrl Pts',(0.404717578595296,-0.0793800000000001,
1.65807299932179));
#13479=CARTESIAN_POINT('Ctrl Pts',(0.400393769631747,-0.101649918886749,
1.65912839404491));
#13480=CARTESIAN_POINT('Ctrl Pts',(0.394174530911058,-0.123823518623745,
1.66063136041479));
#13481=CARTESIAN_POINT('Ctrl Pts',(0.368536561654407,-0.192480977588835,
1.66658649961961));
#13482=CARTESIAN_POINT('Ctrl Pts',(0.341837165343982,-0.236152929235937,
1.67246562047521));
#13483=CARTESIAN_POINT('Ctrl Pts',(0.283214707341173,-0.303141259068211,
1.68332504372461));
#13484=CARTESIAN_POINT('Ctrl Pts',(0.244262842368623,-0.335108247315849,
1.68958170688653));
#13485=CARTESIAN_POINT('Ctrl Pts',(0.178166559972324,-0.373243761060364,
1.69769003172132));
#13486=CARTESIAN_POINT('Ctrl Pts',(0.143648558862931,-0.387888272594439,
1.70107730356824));
#13487=CARTESIAN_POINT('Ctrl Pts',(0.0717778861362652,-0.407041111792943,
1.70562212620408));
#13488=CARTESIAN_POINT('Ctrl Pts',(0.0344244045173309,-0.411552957311693,
1.706752));
#13489=CARTESIAN_POINT('Ctrl Pts',(-0.0344244045173315,-0.411552957311693,
1.706752));
#13490=CARTESIAN_POINT('Ctrl Pts',(-0.0717778861362658,-0.407041111792943,
1.70562212620408));
#13491=CARTESIAN_POINT('Ctrl Pts',(-0.143648558862932,-0.387888272594439,
1.70107730356824));
#13492=CARTESIAN_POINT('Ctrl Pts',(-0.178166559972325,-0.373243761060364,
1.69769003172132));
#13493=CARTESIAN_POINT('Ctrl Pts',(-0.244262842368624,-0.335108247315849,
1.68958170688653));
#13494=CARTESIAN_POINT('Ctrl Pts',(-0.283214707341173,-0.303141259068212,
1.68332504372461));
#13495=CARTESIAN_POINT('Ctrl Pts',(-0.341837165343982,-0.236152929235937,
1.67246562047521));
#13496=CARTESIAN_POINT('Ctrl Pts',(-0.368536561654408,-0.192480977588835,
1.66658649961961));
#13497=CARTESIAN_POINT('Ctrl Pts',(-0.394174530911059,-0.123823518623745,
1.66063136041479));
#13498=CARTESIAN_POINT('Ctrl Pts',(-0.400393769631748,-0.101649918886749,
1.65912839404491));
#13499=CARTESIAN_POINT('Ctrl Pts',(-0.404717578595297,-0.0793800000000001,
1.65807299932179));
#13500=CARTESIAN_POINT('',(-0.886256117232624,-0.07938,1.45861320581289));
#13501=CARTESIAN_POINT('Origin',(0.,-0.07938,0.));
#13502=CARTESIAN_POINT('',(-1.45861320581289,-0.07938,0.886256117232623));
#13503=CARTESIAN_POINT('Ctrl Pts',(-0.886256117232623,-0.0793800000000001,
1.45861320581289));
#13504=CARTESIAN_POINT('Ctrl Pts',(-0.890059788636852,-0.101649918886749,
1.45630208793976));
#13505=CARTESIAN_POINT('Ctrl Pts',(-0.895520212222106,-0.123823518623745,
1.45296717977858));
#13506=CARTESIAN_POINT('Ctrl Pts',(-0.917859913453974,-0.192480977588835,
1.43904931717599));
#13507=CARTESIAN_POINT('Ctrl Pts',(-0.940896403863071,-0.236152929235937,
1.4243271592157));
#13508=CARTESIAN_POINT('Ctrl Pts',(-0.990027513266105,-0.303141259068211,
1.39055359345152));
#13509=CARTESIAN_POINT('Ctrl Pts',(-1.02199477007745,-0.335108247315848,
1.36743459453896));
#13510=CARTESIAN_POINT('Ctrl Pts',(-1.07446535104584,-0.373243761060364,
1.32643091652006));
#13511=CARTESIAN_POINT('Ctrl Pts',(-1.10126842659597,-0.387888272594439,
1.30441816675528));
#13512=CARTESIAN_POINT('Ctrl Pts',(-1.15530234155453,-0.407041111792943,
1.25681160160691));
#13513=CARTESIAN_POINT('Ctrl Pts',(-1.18251418313119,-0.411552957311693,
1.23119764287622));
#13514=CARTESIAN_POINT('Ctrl Pts',(-1.23119764287622,-0.411552957311693,
1.18251418313119));
#13515=CARTESIAN_POINT('Ctrl Pts',(-1.25681160160691,-0.407041111792943,
1.15530234155453));
#13516=CARTESIAN_POINT('Ctrl Pts',(-1.30441816675528,-0.387888272594439,
1.10126842659597));
#13517=CARTESIAN_POINT('Ctrl Pts',(-1.32643091652006,-0.373243761060365,
1.07446535104584));
#13518=CARTESIAN_POINT('Ctrl Pts',(-1.36743459453896,-0.335108247315849,
1.02199477007745));
#13519=CARTESIAN_POINT('Ctrl Pts',(-1.39055359345152,-0.303141259068212,
0.990027513266106));
#13520=CARTESIAN_POINT('Ctrl Pts',(-1.4243271592157,-0.236152929235938,
0.940896403863071));
#13521=CARTESIAN_POINT('Ctrl Pts',(-1.43904931717599,-0.192480977588836,
0.917859913453974));
#13522=CARTESIAN_POINT('Ctrl Pts',(-1.45296717977858,-0.123823518623746,
0.895520212222106));
#13523=CARTESIAN_POINT('Ctrl Pts',(-1.45630208793976,-0.101649918886749,
0.890059788636852));
#13524=CARTESIAN_POINT('Ctrl Pts',(-1.45861320581289,-0.0793800000000001,
0.886256117232623));
#13525=CARTESIAN_POINT('',(-1.65807299932179,-0.07938,0.404717578595295));
#13526=CARTESIAN_POINT('Origin',(0.,-0.07938,0.));
#13527=CARTESIAN_POINT('',(-1.706752,-0.411552957311693,2.08591827245526E-16));
#13528=CARTESIAN_POINT('Ctrl Pts',(-1.65807299932179,-0.0793800000000001,
0.404717578595296));
#13529=CARTESIAN_POINT('Ctrl Pts',(-1.65912839404491,-0.101649918886749,
0.400393769631747));
#13530=CARTESIAN_POINT('Ctrl Pts',(-1.66063136041479,-0.123823518623745,
0.394174530911058));
#13531=CARTESIAN_POINT('Ctrl Pts',(-1.66658649961961,-0.192480977588835,
0.368536561654407));
#13532=CARTESIAN_POINT('Ctrl Pts',(-1.67246562047521,-0.236152929235937,
0.341837165343982));
#13533=CARTESIAN_POINT('Ctrl Pts',(-1.68332504372461,-0.303141259068211,
0.283214707341173));
#13534=CARTESIAN_POINT('Ctrl Pts',(-1.68958170688653,-0.335108247315848,
0.244262842368623));
#13535=CARTESIAN_POINT('Ctrl Pts',(-1.69769003172132,-0.373243761060364,
0.178166559972324));
#13536=CARTESIAN_POINT('Ctrl Pts',(-1.70107730356824,-0.387888272594439,
0.143648558862931));
#13537=CARTESIAN_POINT('Ctrl Pts',(-1.70562212620408,-0.407041111792943,
0.0717778861362656));
#13538=CARTESIAN_POINT('Ctrl Pts',(-1.706752,-0.411552957311693,0.0344244045173313));
#13539=CARTESIAN_POINT('Ctrl Pts',(-1.706752,-0.411552957311693,2.08166817117217E-16));
#13540=CARTESIAN_POINT('',(-1.706752,-0.47628,2.09016837373834E-16));
#13541=CARTESIAN_POINT('',(-1.706752,-0.27783,2.09016837373834E-16));
#13542=CARTESIAN_POINT('Origin',(0.,-0.47628,0.));
#13543=CARTESIAN_POINT('',(-1.65807299932179,-0.07938,-0.404717578595296));
#13544=CARTESIAN_POINT('Ctrl Pts',(-1.706752,-0.411552957311693,2.0122792321331E-16));
#13545=CARTESIAN_POINT('Ctrl Pts',(-1.706752,-0.411552957311693,-0.0344244045173309));
#13546=CARTESIAN_POINT('Ctrl Pts',(-1.70562212620408,-0.407041111792943,
-0.0717778861362652));
#13547=CARTESIAN_POINT('Ctrl Pts',(-1.70107730356824,-0.387888272594439,
-0.143648558862931));
#13548=CARTESIAN_POINT('Ctrl Pts',(-1.69769003172132,-0.373243761060365,
-0.178166559972324));
#13549=CARTESIAN_POINT('Ctrl Pts',(-1.68958170688653,-0.335108247315849,
-0.244262842368623));
#13550=CARTESIAN_POINT('Ctrl Pts',(-1.68332504372461,-0.303141259068212,
-0.283214707341173));
#13551=CARTESIAN_POINT('Ctrl Pts',(-1.67246562047521,-0.236152929235938,
-0.341837165343982));
#13552=CARTESIAN_POINT('Ctrl Pts',(-1.66658649961961,-0.192480977588836,
-0.368536561654407));
#13553=CARTESIAN_POINT('Ctrl Pts',(-1.66063136041479,-0.123823518623745,
-0.394174530911059));
#13554=CARTESIAN_POINT('Ctrl Pts',(-1.65912839404491,-0.101649918886749,
-0.400393769631748));
#13555=CARTESIAN_POINT('Ctrl Pts',(-1.65807299932179,-0.0793800000000001,
-0.404717578595296));
#13556=CARTESIAN_POINT('',(-1.45861320581289,-0.07938,-0.886256117232623));
#13557=CARTESIAN_POINT('Origin',(0.,-0.07938,0.));
#13558=CARTESIAN_POINT('',(-0.886256117232623,-0.07938,-1.45861320581289));
#13559=CARTESIAN_POINT('Ctrl Pts',(-1.45861320581289,-0.0793800000000001,
-0.886256117232623));
#13560=CARTESIAN_POINT('Ctrl Pts',(-1.45630208793976,-0.101649918886749,
-0.890059788636852));
#13561=CARTESIAN_POINT('Ctrl Pts',(-1.45296717977858,-0.123823518623745,
-0.895520212222106));
#13562=CARTESIAN_POINT('Ctrl Pts',(-1.43904931717599,-0.192480977588835,
-0.917859913453974));
#13563=CARTESIAN_POINT('Ctrl Pts',(-1.4243271592157,-0.236152929235937,
-0.940896403863072));
#13564=CARTESIAN_POINT('Ctrl Pts',(-1.39055359345152,-0.303141259068212,
-0.990027513266106));
#13565=CARTESIAN_POINT('Ctrl Pts',(-1.36743459453896,-0.335108247315849,
-1.02199477007745));
#13566=CARTESIAN_POINT('Ctrl Pts',(-1.32643091652006,-0.373243761060364,
-1.07446535104584));
#13567=CARTESIAN_POINT('Ctrl Pts',(-1.30441816675528,-0.387888272594439,
-1.10126842659597));
#13568=CARTESIAN_POINT('Ctrl Pts',(-1.25681160160691,-0.407041111792943,
-1.15530234155453));
#13569=CARTESIAN_POINT('Ctrl Pts',(-1.23119764287622,-0.411552957311693,
-1.18251418313119));
#13570=CARTESIAN_POINT('Ctrl Pts',(-1.18251418313119,-0.411552957311693,
-1.23119764287622));
#13571=CARTESIAN_POINT('Ctrl Pts',(-1.15530234155453,-0.407041111792943,
-1.25681160160691));
#13572=CARTESIAN_POINT('Ctrl Pts',(-1.10126842659597,-0.387888272594439,
-1.30441816675528));
#13573=CARTESIAN_POINT('Ctrl Pts',(-1.07446535104584,-0.373243761060364,
-1.32643091652006));
#13574=CARTESIAN_POINT('Ctrl Pts',(-1.02199477007745,-0.335108247315848,
-1.36743459453896));
#13575=CARTESIAN_POINT('Ctrl Pts',(-0.990027513266105,-0.303141259068211,
-1.39055359345152));
#13576=CARTESIAN_POINT('Ctrl Pts',(-0.940896403863071,-0.236152929235936,
-1.42432715921571));
#13577=CARTESIAN_POINT('Ctrl Pts',(-0.917859913453974,-0.192480977588835,
-1.43904931717599));
#13578=CARTESIAN_POINT('Ctrl Pts',(-0.895520212222106,-0.123823518623745,
-1.45296717977858));
#13579=CARTESIAN_POINT('Ctrl Pts',(-0.890059788636851,-0.101649918886749,
-1.45630208793976));
#13580=CARTESIAN_POINT('Ctrl Pts',(-0.886256117232623,-0.0793800000000001,
-1.45861320581289));
#13581=CARTESIAN_POINT('',(-0.404717578595295,-0.07938,-1.65807299932179));
#13582=CARTESIAN_POINT('Origin',(0.,-0.07938,0.));
#13583=CARTESIAN_POINT('',(0.404717578595296,-0.07938,-1.65807299932179));
#13584=CARTESIAN_POINT('Ctrl Pts',(-0.404717578595296,-0.0793800000000001,
-1.65807299932179));
#13585=CARTESIAN_POINT('Ctrl Pts',(-0.400393769631747,-0.101649918886749,
-1.65912839404491));
#13586=CARTESIAN_POINT('Ctrl Pts',(-0.394174530911058,-0.123823518623746,
-1.66063136041479));
#13587=CARTESIAN_POINT('Ctrl Pts',(-0.368536561654407,-0.192480977588836,
-1.66658649961961));
#13588=CARTESIAN_POINT('Ctrl Pts',(-0.341837165343982,-0.236152929235938,
-1.67246562047521));
#13589=CARTESIAN_POINT('Ctrl Pts',(-0.283214707341173,-0.303141259068212,
-1.68332504372461));
#13590=CARTESIAN_POINT('Ctrl Pts',(-0.244262842368623,-0.335108247315849,
-1.68958170688653));
#13591=CARTESIAN_POINT('Ctrl Pts',(-0.178166559972324,-0.373243761060364,
-1.69769003172132));
#13592=CARTESIAN_POINT('Ctrl Pts',(-0.143648558862931,-0.387888272594439,
-1.70107730356824));
#13593=CARTESIAN_POINT('Ctrl Pts',(-0.0717778861362653,-0.407041111792943,
-1.70562212620408));
#13594=CARTESIAN_POINT('Ctrl Pts',(-0.034424404517331,-0.411552957311693,
-1.706752));
#13595=CARTESIAN_POINT('Ctrl Pts',(0.0344244045173312,-0.411552957311693,
-1.706752));
#13596=CARTESIAN_POINT('Ctrl Pts',(0.0717778861362655,-0.407041111792943,
-1.70562212620408));
#13597=CARTESIAN_POINT('Ctrl Pts',(0.143648558862931,-0.387888272594439,
-1.70107730356824));
#13598=CARTESIAN_POINT('Ctrl Pts',(0.178166559972324,-0.373243761060364,
-1.69769003172132));
#13599=CARTESIAN_POINT('Ctrl Pts',(0.244262842368623,-0.335108247315849,
-1.68958170688653));
#13600=CARTESIAN_POINT('Ctrl Pts',(0.283214707341173,-0.303141259068212,
-1.68332504372461));
#13601=CARTESIAN_POINT('Ctrl Pts',(0.341837165343982,-0.236152929235937,
-1.67246562047521));
#13602=CARTESIAN_POINT('Ctrl Pts',(0.368536561654407,-0.192480977588835,
-1.66658649961961));
#13603=CARTESIAN_POINT('Ctrl Pts',(0.394174530911059,-0.123823518623745,
-1.66063136041479));
#13604=CARTESIAN_POINT('Ctrl Pts',(0.400393769631748,-0.101649918886749,
-1.65912839404491));
#13605=CARTESIAN_POINT('Ctrl Pts',(0.404717578595296,-0.0793800000000001,
-1.65807299932179));
#13606=CARTESIAN_POINT('',(0.886256117232623,-0.07938,-1.45861320581289));
#13607=CARTESIAN_POINT('Origin',(0.,-0.07938,0.));
#13608=CARTESIAN_POINT('',(1.45861320581289,-0.07938,-0.886256117232623));
#13609=CARTESIAN_POINT('Ctrl Pts',(0.886256117232623,-0.0793800000000001,
-1.45861320581289));
#13610=CARTESIAN_POINT('Ctrl Pts',(0.890059788636852,-0.101649918886749,
-1.45630208793976));
#13611=CARTESIAN_POINT('Ctrl Pts',(0.895520212222106,-0.123823518623745,
-1.45296717977858));
#13612=CARTESIAN_POINT('Ctrl Pts',(0.917859913453974,-0.192480977588835,
-1.43904931717599));
#13613=CARTESIAN_POINT('Ctrl Pts',(0.940896403863072,-0.236152929235937,
-1.4243271592157));
#13614=CARTESIAN_POINT('Ctrl Pts',(0.990027513266106,-0.303141259068211,
-1.39055359345152));
#13615=CARTESIAN_POINT('Ctrl Pts',(1.02199477007745,-0.335108247315849,
-1.36743459453896));
#13616=CARTESIAN_POINT('Ctrl Pts',(1.07446535104584,-0.373243761060364,
-1.32643091652006));
#13617=CARTESIAN_POINT('Ctrl Pts',(1.10126842659597,-0.387888272594439,
-1.30441816675528));
#13618=CARTESIAN_POINT('Ctrl Pts',(1.15530234155453,-0.407041111792943,
-1.25681160160691));
#13619=CARTESIAN_POINT('Ctrl Pts',(1.18251418313119,-0.411552957311693,
-1.23119764287622));
#13620=CARTESIAN_POINT('Ctrl Pts',(1.23119764287622,-0.411552957311693,
-1.18251418313119));
#13621=CARTESIAN_POINT('Ctrl Pts',(1.25681160160691,-0.407041111792943,
-1.15530234155453));
#13622=CARTESIAN_POINT('Ctrl Pts',(1.30441816675528,-0.387888272594439,
-1.10126842659597));
#13623=CARTESIAN_POINT('Ctrl Pts',(1.32643091652006,-0.373243761060364,
-1.07446535104584));
#13624=CARTESIAN_POINT('Ctrl Pts',(1.36743459453896,-0.335108247315849,
-1.02199477007745));
#13625=CARTESIAN_POINT('Ctrl Pts',(1.39055359345152,-0.303141259068212,
-0.990027513266105));
#13626=CARTESIAN_POINT('Ctrl Pts',(1.4243271592157,-0.236152929235937,-0.940896403863071));
#13627=CARTESIAN_POINT('Ctrl Pts',(1.43904931717599,-0.192480977588835,
-0.917859913453974));
#13628=CARTESIAN_POINT('Ctrl Pts',(1.45296717977858,-0.123823518623745,
-0.895520212222106));
#13629=CARTESIAN_POINT('Ctrl Pts',(1.45630208793976,-0.101649918886749,
-0.890059788636852));
#13630=CARTESIAN_POINT('Ctrl Pts',(1.45861320581289,-0.0793800000000001,
-0.886256117232623));
#13631=CARTESIAN_POINT('',(1.65807299932179,-0.07938,-0.404717578595296));
#13632=CARTESIAN_POINT('Origin',(0.,-0.07938,0.));
#13633=CARTESIAN_POINT('',(1.65807299932179,-0.07938,0.404717578595296));
#13634=CARTESIAN_POINT('Ctrl Pts',(1.65807299932179,-0.0793800000000001,
-0.404717578595296));
#13635=CARTESIAN_POINT('Ctrl Pts',(1.65912839404491,-0.101649918886749,
-0.400393769631747));
#13636=CARTESIAN_POINT('Ctrl Pts',(1.66063136041479,-0.123823518623745,
-0.394174530911058));
#13637=CARTESIAN_POINT('Ctrl Pts',(1.66658649961961,-0.192480977588835,
-0.368536561654407));
#13638=CARTESIAN_POINT('Ctrl Pts',(1.67246562047521,-0.236152929235937,
-0.341837165343982));
#13639=CARTESIAN_POINT('Ctrl Pts',(1.68332504372461,-0.303141259068212,
-0.283214707341173));
#13640=CARTESIAN_POINT('Ctrl Pts',(1.68958170688653,-0.335108247315849,
-0.244262842368623));
#13641=CARTESIAN_POINT('Ctrl Pts',(1.69769003172132,-0.373243761060364,
-0.178166559972324));
#13642=CARTESIAN_POINT('Ctrl Pts',(1.70107730356824,-0.387888272594439,
-0.143648558862931));
#13643=CARTESIAN_POINT('Ctrl Pts',(1.70562212620408,-0.407041111792943,
-0.0717778861362655));
#13644=CARTESIAN_POINT('Ctrl Pts',(1.706752,-0.411552957311693,-0.0344244045173312));
#13645=CARTESIAN_POINT('Ctrl Pts',(1.706752,-0.411552957311693,0.0344244045173312));
#13646=CARTESIAN_POINT('Ctrl Pts',(1.70562212620408,-0.407041111792943,
0.0717778861362655));
#13647=CARTESIAN_POINT('Ctrl Pts',(1.70107730356824,-0.387888272594439,
0.143648558862931));
#13648=CARTESIAN_POINT('Ctrl Pts',(1.69769003172132,-0.373243761060364,
0.178166559972324));
#13649=CARTESIAN_POINT('Ctrl Pts',(1.68958170688653,-0.335108247315849,
0.244262842368623));
#13650=CARTESIAN_POINT('Ctrl Pts',(1.68332504372461,-0.303141259068212,
0.283214707341173));
#13651=CARTESIAN_POINT('Ctrl Pts',(1.67246562047521,-0.236152929235937,
0.341837165343982));
#13652=CARTESIAN_POINT('Ctrl Pts',(1.66658649961961,-0.192480977588835,
0.368536561654407));
#13653=CARTESIAN_POINT('Ctrl Pts',(1.66063136041479,-0.123823518623745,
0.394174530911058));
#13654=CARTESIAN_POINT('Ctrl Pts',(1.65912839404491,-0.101649918886749,
0.400393769631747));
#13655=CARTESIAN_POINT('Ctrl Pts',(1.65807299932179,-0.0793800000000001,
0.404717578595296));
#13656=CARTESIAN_POINT('Origin',(0.,-0.07938,0.));
#13657=CARTESIAN_POINT('Origin',(0.,-0.07938,0.));
#13658=CARTESIAN_POINT('',(0.397005914195118,-0.07938,1.59456899932179));
#13659=CARTESIAN_POINT('Origin',(0.,-0.07938,0.));
#13660=CARTESIAN_POINT('Origin',(-3.33066907387547E-16,-0.07938,1.675));
#13661=CARTESIAN_POINT('Origin',(-3.33066907387547E-16,0.,1.675));
#13662=CARTESIAN_POINT('',(-0.397005914195118,-0.07938,1.59456899932179));
#13663=CARTESIAN_POINT('Ctrl Pts',(-0.397005914195119,-0.0793800000000001,
1.59456899932179));
#13664=CARTESIAN_POINT('Ctrl Pts',(-0.3886265584581,-0.123401821157026,
1.59665523941937));
#13665=CARTESIAN_POINT('Ctrl Pts',(-0.373030350867485,-0.166543350814306,
1.60050712143809));
#13666=CARTESIAN_POINT('Ctrl Pts',(-0.333298652394954,-0.237231147975234,
1.60919314384089));
#13667=CARTESIAN_POINT('Ctrl Pts',(-0.311480544243687,-0.266264900654909,
1.61365775139403));
#13668=CARTESIAN_POINT('Ctrl Pts',(-0.261368388670537,-0.317195968905306,
1.62252828437015));
#13669=CARTESIAN_POINT('Ctrl Pts',(-0.233069203882014,-0.33909093068465,
1.62691869420078));
#13670=CARTESIAN_POINT('Ctrl Pts',(-0.174042761838764,-0.373586846396559,
1.63426473152765));
#13671=CARTESIAN_POINT('Ctrl Pts',(-0.14036578147155,-0.388086240756494,
1.63761964365402));
#13672=CARTESIAN_POINT('Ctrl Pts',(-0.0701778381840615,-0.407068917407805,
1.64212536811722));
#13673=CARTESIAN_POINT('Ctrl Pts',(-0.0336652739555918,-0.411552957311693,
1.643248));
#13674=CARTESIAN_POINT('Ctrl Pts',(0.0336652739555913,-0.411552957311693,
1.643248));
#13675=CARTESIAN_POINT('Ctrl Pts',(0.070177838184061,-0.407068917407805,
1.64212536811722));
#13676=CARTESIAN_POINT('Ctrl Pts',(0.140365781471549,-0.388086240756494,
1.63761964365402));
#13677=CARTESIAN_POINT('Ctrl Pts',(0.174042761838763,-0.373586846396559,
1.63426473152765));
#13678=CARTESIAN_POINT('Ctrl Pts',(0.233069203882014,-0.33909093068465,
1.62691869420078));
#13679=CARTESIAN_POINT('Ctrl Pts',(0.261368388670536,-0.317195968905306,
1.62252828437015));
#13680=CARTESIAN_POINT('Ctrl Pts',(0.311480544243686,-0.266264900654908,
1.61365775139403));
#13681=CARTESIAN_POINT('Ctrl Pts',(0.333298652394954,-0.237231147975234,
1.60919314384089));
#13682=CARTESIAN_POINT('Ctrl Pts',(0.373030350867484,-0.166543350814306,
1.60050712143809));
#13683=CARTESIAN_POINT('Ctrl Pts',(0.388626558458099,-0.123401821157026,
1.59665523941937));
#13684=CARTESIAN_POINT('Ctrl Pts',(0.397005914195118,-0.07938,1.59456899932179));
#13685=CARTESIAN_POINT('Origin',(-3.33066907387547E-16,-0.07938,1.675));
#13686=CARTESIAN_POINT('Origin',(0.,-0.07938,0.));
#13687=CARTESIAN_POINT('',(-0.846804978391754,-0.07938,1.40825612658882));
#13688=CARTESIAN_POINT('Origin',(0.,-0.07938,0.));
#13689=CARTESIAN_POINT('Origin',(-1.18440385848747,-0.07938,1.18440385848747));
#13690=CARTESIAN_POINT('Origin',(-1.18440385848747,0.,1.18440385848747));
#13691=CARTESIAN_POINT('',(-1.40825612658882,-0.07938,0.846804978391753));
#13692=CARTESIAN_POINT('Ctrl Pts',(-1.40825612658882,-0.0793800000000001,
0.846804978391753));
#13693=CARTESIAN_POINT('Ctrl Pts',(-1.40380622184538,-0.123401821157026,
0.854205272175555));
#13694=CARTESIAN_POINT('Ctrl Pts',(-1.39550172959303,-0.166543350814306,
0.867957148219442));
#13695=CARTESIAN_POINT('Ctrl Pts',(-1.3735491215176,-0.237231147975235,
0.902193646979983));
#13696=CARTESIAN_POINT('Ctrl Pts',(-1.36127834356734,-0.266264900654909,
0.920778333482565));
#13697=CARTESIAN_POINT('Ctrl Pts',(-1.33211611256184,-0.317195968905306,
0.962485392528369));
#13698=CARTESIAN_POINT('Ctrl Pts',(-1.31521005565926,-0.339090930684651,
0.985600426557816));
#13699=CARTESIAN_POINT('Ctrl Pts',(-1.27866649102984,-0.373586846396559,
1.03253285680459));
#13700=CARTESIAN_POINT('Ctrl Pts',(-1.25722555095714,-0.388086240756494,
1.05871835910697));
#13701=CARTESIAN_POINT('Ctrl Pts',(-1.2107812086231,-0.407068917407805,
1.11153475808518));
#13702=CARTESIAN_POINT('Ctrl Pts',(-1.18575674747573,-0.411552957311693,
1.13814686046673));
#13703=CARTESIAN_POINT('Ctrl Pts',(-1.13814686046673,-0.411552957311693,
1.18575674747573));
#13704=CARTESIAN_POINT('Ctrl Pts',(-1.11153475808518,-0.407068917407805,
1.2107812086231));
#13705=CARTESIAN_POINT('Ctrl Pts',(-1.05871835910697,-0.388086240756494,
1.25722555095714));
#13706=CARTESIAN_POINT('Ctrl Pts',(-1.03253285680459,-0.373586846396559,
1.27866649102984));
#13707=CARTESIAN_POINT('Ctrl Pts',(-0.985600426557816,-0.33909093068465,
1.31521005565926));
#13708=CARTESIAN_POINT('Ctrl Pts',(-0.962485392528369,-0.317195968905306,
1.33211611256184));
#13709=CARTESIAN_POINT('Ctrl Pts',(-0.920778333482565,-0.266264900654908,
1.36127834356734));
#13710=CARTESIAN_POINT('Ctrl Pts',(-0.902193646979983,-0.237231147975234,
1.3735491215176));
#13711=CARTESIAN_POINT('Ctrl Pts',(-0.867957148219442,-0.166543350814306,
1.39550172959303));
#13712=CARTESIAN_POINT('Ctrl Pts',(-0.854205272175555,-0.123401821157026,
1.40380622184538));
#13713=CARTESIAN_POINT('Ctrl Pts',(-0.846804978391753,-0.0793800000000001,
1.40825612658882));
#13714=CARTESIAN_POINT('Origin',(-1.18440385848747,-0.07938,1.18440385848747));
#13715=CARTESIAN_POINT('Origin',(0.,-0.07938,0.));
#13716=CARTESIAN_POINT('',(-1.59456899932179,-0.07938,0.397005914195118));
#13717=CARTESIAN_POINT('Origin',(0.,-0.07938,0.));
#13718=CARTESIAN_POINT('Origin',(-1.675,-0.07938,-2.22044604925031E-16));
#13719=CARTESIAN_POINT('Origin',(-1.675,0.,-2.22044604925031E-16));
#13720=CARTESIAN_POINT('',(-1.59456899932179,-0.07938,-0.397005914195118));
#13721=CARTESIAN_POINT('',(-1.643248,-0.411552957311693,3.47540551556327E-18));
#13722=CARTESIAN_POINT('Ctrl Pts',(-1.59456899932179,-0.0793800000000001,
-0.397005914195119));
#13723=CARTESIAN_POINT('Ctrl Pts',(-1.59665523941937,-0.123401821157026,
-0.388626558458099));
#13724=CARTESIAN_POINT('Ctrl Pts',(-1.60050712143809,-0.166543350814306,
-0.373030350867485));
#13725=CARTESIAN_POINT('Ctrl Pts',(-1.60919314384089,-0.237231147975234,
-0.333298652394954));
#13726=CARTESIAN_POINT('Ctrl Pts',(-1.61365775139403,-0.266264900654909,
-0.311480544243686));
#13727=CARTESIAN_POINT('Ctrl Pts',(-1.62252828437015,-0.317195968905306,
-0.261368388670537));
#13728=CARTESIAN_POINT('Ctrl Pts',(-1.62691869420078,-0.33909093068465,
-0.233069203882014));
#13729=CARTESIAN_POINT('Ctrl Pts',(-1.63426473152765,-0.373586846396559,
-0.174042761838764));
#13730=CARTESIAN_POINT('Ctrl Pts',(-1.63761964365402,-0.388086240756494,
-0.140365781471549));
#13731=CARTESIAN_POINT('Ctrl Pts',(-1.64212536811722,-0.407068917407805,
-0.0701778381840614));
#13732=CARTESIAN_POINT('Ctrl Pts',(-1.643248,-0.411552957311693,-0.0336652739555917));
#13733=CARTESIAN_POINT('Ctrl Pts',(-1.643248,-0.411552957311693,-2.0122792321331E-16));
#13734=CARTESIAN_POINT('Origin',(-1.675,-0.07938,-2.22044604925031E-16));
#13735=CARTESIAN_POINT('Ctrl Pts',(-1.643248,-0.411552957311693,-1.94289029309402E-16));
#13736=CARTESIAN_POINT('Ctrl Pts',(-1.643248,-0.411552957311693,0.0336652739555913));
#13737=CARTESIAN_POINT('Ctrl Pts',(-1.64212536811722,-0.407068917407805,
0.0701778381840609));
#13738=CARTESIAN_POINT('Ctrl Pts',(-1.63761964365402,-0.388086240756494,
0.140365781471549));
#13739=CARTESIAN_POINT('Ctrl Pts',(-1.63426473152765,-0.373586846396559,
0.174042761838763));
#13740=CARTESIAN_POINT('Ctrl Pts',(-1.62691869420078,-0.33909093068465,
0.233069203882014));
#13741=CARTESIAN_POINT('Ctrl Pts',(-1.62252828437015,-0.317195968905306,
0.261368388670536));
#13742=CARTESIAN_POINT('Ctrl Pts',(-1.61365775139403,-0.266264900654909,
0.311480544243686));
#13743=CARTESIAN_POINT('Ctrl Pts',(-1.60919314384089,-0.237231147975235,
0.333298652394954));
#13744=CARTESIAN_POINT('Ctrl Pts',(-1.60050712143809,-0.166543350814306,
0.373030350867484));
#13745=CARTESIAN_POINT('Ctrl Pts',(-1.59665523941937,-0.123401821157026,
0.388626558458099));
#13746=CARTESIAN_POINT('Ctrl Pts',(-1.59456899932179,-0.0793800000000001,
0.397005914195118));
#13747=CARTESIAN_POINT('Origin',(0.,-0.07938,0.));
#13748=CARTESIAN_POINT('',(-1.40825612658882,-0.07938,-0.846804978391753));
#13749=CARTESIAN_POINT('Origin',(0.,-0.07938,0.));
#13750=CARTESIAN_POINT('Origin',(-1.18440385848747,-0.07938,-1.18440385848747));
#13751=CARTESIAN_POINT('Origin',(-1.18440385848747,0.,-1.18440385848747));
#13752=CARTESIAN_POINT('',(-0.846804978391753,-0.07938,-1.40825612658882));
#13753=CARTESIAN_POINT('Ctrl Pts',(-0.846804978391753,-0.0793800000000001,
-1.40825612658882));
#13754=CARTESIAN_POINT('Ctrl Pts',(-0.854205272175555,-0.123401821157026,
-1.40380622184538));
#13755=CARTESIAN_POINT('Ctrl Pts',(-0.867957148219442,-0.166543350814306,
-1.39550172959303));
#13756=CARTESIAN_POINT('Ctrl Pts',(-0.902193646979982,-0.237231147975234,
-1.3735491215176));
#13757=CARTESIAN_POINT('Ctrl Pts',(-0.920778333482564,-0.266264900654908,
-1.36127834356734));
#13758=CARTESIAN_POINT('Ctrl Pts',(-0.962485392528368,-0.317195968905306,
-1.33211611256184));
#13759=CARTESIAN_POINT('Ctrl Pts',(-0.985600426557816,-0.33909093068465,
-1.31521005565926));
#13760=CARTESIAN_POINT('Ctrl Pts',(-1.03253285680459,-0.373586846396559,
-1.27866649102984));
#13761=CARTESIAN_POINT('Ctrl Pts',(-1.05871835910697,-0.388086240756494,
-1.25722555095714));
#13762=CARTESIAN_POINT('Ctrl Pts',(-1.11153475808518,-0.407068917407805,
-1.2107812086231));
#13763=CARTESIAN_POINT('Ctrl Pts',(-1.13814686046673,-0.411552957311693,
-1.18575674747573));
#13764=CARTESIAN_POINT('Ctrl Pts',(-1.18575674747573,-0.411552957311693,
-1.13814686046673));
#13765=CARTESIAN_POINT('Ctrl Pts',(-1.2107812086231,-0.407068917407805,
-1.11153475808518));
#13766=CARTESIAN_POINT('Ctrl Pts',(-1.25722555095714,-0.388086240756494,
-1.05871835910697));
#13767=CARTESIAN_POINT('Ctrl Pts',(-1.27866649102984,-0.373586846396559,
-1.03253285680459));
#13768=CARTESIAN_POINT('Ctrl Pts',(-1.31521005565926,-0.33909093068465,
-0.985600426557816));
#13769=CARTESIAN_POINT('Ctrl Pts',(-1.33211611256184,-0.317195968905306,
-0.962485392528369));
#13770=CARTESIAN_POINT('Ctrl Pts',(-1.36127834356734,-0.266264900654909,
-0.920778333482565));
#13771=CARTESIAN_POINT('Ctrl Pts',(-1.3735491215176,-0.237231147975234,
-0.902193646979983));
#13772=CARTESIAN_POINT('Ctrl Pts',(-1.39550172959303,-0.166543350814306,
-0.867957148219442));
#13773=CARTESIAN_POINT('Ctrl Pts',(-1.40380622184538,-0.123401821157026,
-0.854205272175555));
#13774=CARTESIAN_POINT('Ctrl Pts',(-1.40825612658882,-0.07938,-0.846804978391753));
#13775=CARTESIAN_POINT('Origin',(-1.18440385848747,-0.07938,-1.18440385848747));
#13776=CARTESIAN_POINT('Origin',(0.,-0.07938,0.));
#13777=CARTESIAN_POINT('',(-0.397005914195118,-0.07938,-1.59456899932179));
#13778=CARTESIAN_POINT('Origin',(0.,-0.07938,0.));
#13779=CARTESIAN_POINT('Origin',(1.11022302462516E-16,-0.07938,-1.675));
#13780=CARTESIAN_POINT('Origin',(1.11022302462516E-16,0.,-1.675));
#13781=CARTESIAN_POINT('',(0.397005914195118,-0.07938,-1.59456899932179));
#13782=CARTESIAN_POINT('Ctrl Pts',(0.397005914195119,-0.0793800000000001,
-1.59456899932179));
#13783=CARTESIAN_POINT('Ctrl Pts',(0.388626558458099,-0.123401821157026,
-1.59665523941937));
#13784=CARTESIAN_POINT('Ctrl Pts',(0.373030350867485,-0.166543350814306,
-1.60050712143809));
#13785=CARTESIAN_POINT('Ctrl Pts',(0.333298652394954,-0.237231147975234,
-1.60919314384089));
#13786=CARTESIAN_POINT('Ctrl Pts',(0.311480544243686,-0.266264900654909,
-1.61365775139403));
#13787=CARTESIAN_POINT('Ctrl Pts',(0.261368388670537,-0.317195968905306,
-1.62252828437015));
#13788=CARTESIAN_POINT('Ctrl Pts',(0.233069203882014,-0.33909093068465,
-1.62691869420078));
#13789=CARTESIAN_POINT('Ctrl Pts',(0.174042761838763,-0.373586846396559,
-1.63426473152765));
#13790=CARTESIAN_POINT('Ctrl Pts',(0.140365781471549,-0.388086240756494,
-1.63761964365402));
#13791=CARTESIAN_POINT('Ctrl Pts',(0.0701778381840612,-0.407068917407805,
-1.64212536811722));
#13792=CARTESIAN_POINT('Ctrl Pts',(0.0336652739555916,-0.411552957311693,
-1.643248));
#13793=CARTESIAN_POINT('Ctrl Pts',(-0.0336652739555915,-0.411552957311693,
-1.643248));
#13794=CARTESIAN_POINT('Ctrl Pts',(-0.0701778381840612,-0.407068917407805,
-1.64212536811722));
#13795=CARTESIAN_POINT('Ctrl Pts',(-0.140365781471549,-0.388086240756494,
-1.63761964365402));
#13796=CARTESIAN_POINT('Ctrl Pts',(-0.174042761838764,-0.373586846396559,
-1.63426473152765));
#13797=CARTESIAN_POINT('Ctrl Pts',(-0.233069203882014,-0.33909093068465,
-1.62691869420078));
#13798=CARTESIAN_POINT('Ctrl Pts',(-0.261368388670536,-0.317195968905306,
-1.62252828437015));
#13799=CARTESIAN_POINT('Ctrl Pts',(-0.311480544243686,-0.266264900654908,
-1.61365775139403));
#13800=CARTESIAN_POINT('Ctrl Pts',(-0.333298652394954,-0.237231147975234,
-1.60919314384089));
#13801=CARTESIAN_POINT('Ctrl Pts',(-0.373030350867485,-0.166543350814306,
-1.60050712143809));
#13802=CARTESIAN_POINT('Ctrl Pts',(-0.388626558458099,-0.123401821157026,
-1.59665523941937));
#13803=CARTESIAN_POINT('Ctrl Pts',(-0.397005914195118,-0.07938,-1.59456899932179));
#13804=CARTESIAN_POINT('Origin',(1.11022302462516E-16,-0.07938,-1.675));
#13805=CARTESIAN_POINT('Origin',(0.,-0.07938,0.));
#13806=CARTESIAN_POINT('',(0.846804978391753,-0.07938,-1.40825612658882));
#13807=CARTESIAN_POINT('Origin',(0.,-0.07938,0.));
#13808=CARTESIAN_POINT('Origin',(1.18440385848747,-0.07938,-1.18440385848747));
#13809=CARTESIAN_POINT('Origin',(1.18440385848747,0.,-1.18440385848747));
#13810=CARTESIAN_POINT('',(1.40825612658882,-0.07938,-0.846804978391753));
#13811=CARTESIAN_POINT('Ctrl Pts',(1.40825612658882,-0.0793800000000001,
-0.846804978391753));
#13812=CARTESIAN_POINT('Ctrl Pts',(1.40380622184538,-0.123401821157026,
-0.854205272175555));
#13813=CARTESIAN_POINT('Ctrl Pts',(1.39550172959303,-0.166543350814306,
-0.867957148219442));
#13814=CARTESIAN_POINT('Ctrl Pts',(1.3735491215176,-0.237231147975234,-0.902193646979983));
#13815=CARTESIAN_POINT('Ctrl Pts',(1.36127834356734,-0.266264900654908,
-0.920778333482565));
#13816=CARTESIAN_POINT('Ctrl Pts',(1.33211611256184,-0.317195968905306,
-0.962485392528369));
#13817=CARTESIAN_POINT('Ctrl Pts',(1.31521005565926,-0.33909093068465,-0.985600426557816));
#13818=CARTESIAN_POINT('Ctrl Pts',(1.27866649102984,-0.373586846396559,
-1.03253285680459));
#13819=CARTESIAN_POINT('Ctrl Pts',(1.25722555095714,-0.388086240756494,
-1.05871835910697));
#13820=CARTESIAN_POINT('Ctrl Pts',(1.2107812086231,-0.407068917407805,-1.11153475808518));
#13821=CARTESIAN_POINT('Ctrl Pts',(1.18575674747573,-0.411552957311693,
-1.13814686046673));
#13822=CARTESIAN_POINT('Ctrl Pts',(1.13814686046673,-0.411552957311693,
-1.18575674747573));
#13823=CARTESIAN_POINT('Ctrl Pts',(1.11153475808518,-0.407068917407805,
-1.2107812086231));
#13824=CARTESIAN_POINT('Ctrl Pts',(1.05871835910697,-0.388086240756494,
-1.25722555095714));
#13825=CARTESIAN_POINT('Ctrl Pts',(1.03253285680459,-0.373586846396559,
-1.27866649102984));
#13826=CARTESIAN_POINT('Ctrl Pts',(0.985600426557816,-0.33909093068465,
-1.31521005565926));
#13827=CARTESIAN_POINT('Ctrl Pts',(0.962485392528369,-0.317195968905306,
-1.33211611256184));
#13828=CARTESIAN_POINT('Ctrl Pts',(0.920778333482565,-0.266264900654909,
-1.36127834356734));
#13829=CARTESIAN_POINT('Ctrl Pts',(0.902193646979983,-0.237231147975234,
-1.3735491215176));
#13830=CARTESIAN_POINT('Ctrl Pts',(0.867957148219442,-0.166543350814306,
-1.39550172959303));
#13831=CARTESIAN_POINT('Ctrl Pts',(0.854205272175555,-0.123401821157026,
-1.40380622184538));
#13832=CARTESIAN_POINT('Ctrl Pts',(0.846804978391753,-0.0793800000000001,
-1.40825612658882));
#13833=CARTESIAN_POINT('Origin',(1.18440385848747,-0.07938,-1.18440385848747));
#13834=CARTESIAN_POINT('Origin',(0.,-0.27783,0.));
#13835=CARTESIAN_POINT('',(-1.643248,-0.47628,2.01239840340529E-16));
#13836=CARTESIAN_POINT('Origin',(0.,-0.47628,0.));
#13837=CARTESIAN_POINT('',(-1.643248,-0.27783,2.01239840340529E-16));
#13838=CARTESIAN_POINT('',(1.59456899932179,-0.07938,0.397005914195118));
#13839=CARTESIAN_POINT('Origin',(0.,-0.07938,0.));
#13840=CARTESIAN_POINT('',(1.59456899932179,-0.07938,-0.397005914195118));
#13841=CARTESIAN_POINT('Ctrl Pts',(1.59456899932179,-0.0793800000000001,
0.397005914195118));
#13842=CARTESIAN_POINT('Ctrl Pts',(1.59665523941937,-0.123401821157026,
0.388626558458099));
#13843=CARTESIAN_POINT('Ctrl Pts',(1.60050712143809,-0.166543350814306,
0.373030350867485));
#13844=CARTESIAN_POINT('Ctrl Pts',(1.60919314384089,-0.237231147975234,
0.333298652394954));
#13845=CARTESIAN_POINT('Ctrl Pts',(1.61365775139403,-0.266264900654909,
0.311480544243686));
#13846=CARTESIAN_POINT('Ctrl Pts',(1.62252828437015,-0.317195968905306,
0.261368388670537));
#13847=CARTESIAN_POINT('Ctrl Pts',(1.62691869420078,-0.33909093068465,0.233069203882014));
#13848=CARTESIAN_POINT('Ctrl Pts',(1.63426473152765,-0.373586846396559,
0.174042761838764));
#13849=CARTESIAN_POINT('Ctrl Pts',(1.63761964365402,-0.388086240756494,
0.140365781471549));
#13850=CARTESIAN_POINT('Ctrl Pts',(1.64212536811722,-0.407068917407805,
0.0701778381840612));
#13851=CARTESIAN_POINT('Ctrl Pts',(1.643248,-0.411552957311693,0.0336652739555916));
#13852=CARTESIAN_POINT('Ctrl Pts',(1.643248,-0.411552957311693,-0.0336652739555916));
#13853=CARTESIAN_POINT('Ctrl Pts',(1.64212536811722,-0.407068917407805,
-0.0701778381840612));
#13854=CARTESIAN_POINT('Ctrl Pts',(1.63761964365402,-0.388086240756494,
-0.140365781471549));
#13855=CARTESIAN_POINT('Ctrl Pts',(1.63426473152765,-0.373586846396559,
-0.174042761838764));
#13856=CARTESIAN_POINT('Ctrl Pts',(1.62691869420078,-0.33909093068465,-0.233069203882014));
#13857=CARTESIAN_POINT('Ctrl Pts',(1.62252828437015,-0.317195968905306,
-0.261368388670537));
#13858=CARTESIAN_POINT('Ctrl Pts',(1.61365775139403,-0.266264900654909,
-0.311480544243686));
#13859=CARTESIAN_POINT('Ctrl Pts',(1.60919314384089,-0.237231147975234,
-0.333298652394954));
#13860=CARTESIAN_POINT('Ctrl Pts',(1.60050712143809,-0.166543350814306,
-0.373030350867485));
#13861=CARTESIAN_POINT('Ctrl Pts',(1.59665523941937,-0.123401821157026,
-0.388626558458099));
#13862=CARTESIAN_POINT('Ctrl Pts',(1.59456899932179,-0.07938,-0.397005914195118));
#13863=CARTESIAN_POINT('Origin',(0.,-0.07938,0.));
#13864=CARTESIAN_POINT('Origin',(0.,-0.07938,0.));
#13865=CARTESIAN_POINT('Origin',(1.675,-0.07938,0.));
#13866=CARTESIAN_POINT('Origin',(1.675,0.,0.));
#13867=CARTESIAN_POINT('Origin',(1.675,-0.07938,0.));
#13868=CARTESIAN_POINT('Origin',(0.,-0.47628,0.));
#13869=CARTESIAN_POINT('Origin',(0.,-0.07938,0.));
#14761=UNCERTAINTY_MEASURE_WITH_UNIT(LENGTH_MEASURE(0.001),#14823,
'DISTANCE_ACCURACY_VALUE',
'Maximum model space distance between geometric entities at asserted c
onnectivities');
#14777=UNCERTAINTY_MEASURE_WITH_UNIT(LENGTH_MEASURE(0.001),#14823,
'DISTANCE_ACCURACY_VALUE',
'Maximum model space distance between geometric entities at asserted c
onnectivities');
#14806=(
GEOMETRIC_REPRESENTATION_CONTEXT(3)
GLOBAL_UNCERTAINTY_ASSIGNED_CONTEXT((#14761))
GLOBAL_UNIT_ASSIGNED_CONTEXT((#14823,#14825,#14826))
REPRESENTATION_CONTEXT('','3D')
);
#14822=(
GEOMETRIC_REPRESENTATION_CONTEXT(3)
GLOBAL_UNCERTAINTY_ASSIGNED_CONTEXT((#14777))
GLOBAL_UNIT_ASSIGNED_CONTEXT((#14823,#14825,#14826))
REPRESENTATION_CONTEXT('','3D')
);
#14823=(
LENGTH_UNIT()
NAMED_UNIT(*)
SI_UNIT(.CENTI.,.METRE.)
);
#14825=(
NAMED_UNIT(*)
PLANE_ANGLE_UNIT()
SI_UNIT($,.RADIAN.)
);
#14826=(
NAMED_UNIT(*)
SI_UNIT($,.STERADIAN.)
SOLID_ANGLE_UNIT()
);
#14855=SHAPE_DEFINITION_REPRESENTATION(#14904,#15026);
#14904=PRODUCT_DEFINITION_SHAPE('',$,#15071);
#15026=SHAPE_REPRESENTATION('',(#8808),#14806);
#15042=PRODUCT_DEFINITION_CONTEXT('part definition',#15176,'design');
#15071=PRODUCT_DEFINITION('Cage (1)','Cage (1)',#15115,#15042);
#15115=PRODUCT_DEFINITION_FORMATION('',$,#15206);
#15176=APPLICATION_CONTEXT(
'Core Data for Automotive Mechanical Design Process');
#15177=PRODUCT_CONTEXT('part definition',#15176,'mechanical');
#15206=PRODUCT('Cage (1)','Cage (1)','Cage (1)',(#15177));
#15278=COLOUR_RGB('Grey',0.48,0.52,0.57);
#15279=FILL_AREA_STYLE_COLOUR('',#15278);
#15280=FILL_AREA_STYLE('',(#15279));
#15281=SURFACE_STYLE_FILL_AREA(#15280);
#15282=SURFACE_SIDE_STYLE('',(#15281));
#15283=SURFACE_STYLE_USAGE(.BOTH.,#15282);
#15284=PRESENTATION_STYLE_ASSIGNMENT((#15283));
ENDSEC;
END-ISO-10303-21;
